ISO-10303-21;
HEADER;
/* Generated by software containing ST-Developer
 * from STEP Tools, Inc. (www.steptools.com) 
 */

FILE_DESCRIPTION(
/* description */ ('Torque wrench calibration arm'),
/* implementation_level */ '2;1');

FILE_NAME(
/* name */ 'Cage (1).step',
/* time_stamp */ '2026-10-28T03:24:52-07:00',
/* author */ (''),
/* organization */ (''),
/* preprocessor_version */ 'ST-DEVELOPER v20.2',
/* originating_system */ 'Autodesk Translation Framework v15.17.0.0',
/* authorisation */ '');

FILE_SCHEMA (('AUTOMOTIVE_DESIGN { 1 0 10303 214 3 1 1 }'));
ENDSEC;

DATA;
#10=MECHANICAL_DESIGN_GEOMETRIC_PRESENTATION_REPRESENTATION('',(#468),#12783);
#275=B_SPLINE_CURVE_WITH_KNOTS('',3,(#11943,#11944,#11945,#11946,#11947,
#11948,#11949,#11950,#11951,#11952,#11953,#11954,#11955,#11956,#11957,#11958,
#11959,#11960,#11961,#11962,#11963,#11964),.UNSPECIFIED.,.F.,.F.,(4,2,2,
2,2,2,2,2,2,2,4),(0.0473477652366656,0.126350602536658,0.189525903804987,
0.252701205073317,0.313298422430275,0.373895639787233,0.434492857144191,
0.495090074501149,0.558265375769478,0.621440677037807,0.7004435143378),
 .UNSPECIFIED.);
#276=B_SPLINE_CURVE_WITH_KNOTS('',3,(#11968,#11969,#11970,#11971,#11972,
#11973,#11974,#11975,#11976,#11977,#11978,#11979,#11980,#11981,#11982,#11983,
#11984,#11985,#11986,#11987,#11988,#11989),.UNSPECIFIED.,.F.,.F.,(4,2,2,
2,2,2,2,2,2,2,4),(0.0464897534940957,0.0852567806515119,0.170513561303024,
0.246687263103517,0.308657850341199,0.370628437578881,0.432599024816563,
0.494569612054245,0.570743313854739,0.656000094506251,0.694767121663666),
 .UNSPECIFIED.);
#277=B_SPLINE_CURVE_WITH_KNOTS('',3,(#11995,#11996,#11997,#11998,#11999,
#12000,#12001,#12002,#12003,#12004,#12005,#12006,#12007,#12008,#12009,#12010,
#12011,#12012,#12013,#12014,#12015,#12016),.UNSPECIFIED.,.F.,.F.,(4,2,2,
2,2,2,2,2,2,2,4),(0.0464897534940957,0.0852567806515118,0.170513561303024,
0.246687263103517,0.308657850341199,0.370628437578881,0.432599024816563,
0.494569612054245,0.570743313854738,0.65600009450625,0.694767121663666),
 .UNSPECIFIED.);
#278=B_SPLINE_CURVE_WITH_KNOTS('',3,(#12020,#12021,#12022,#12023,#12024,
#12025,#12026,#12027,#12028,#12029,#12030,#12031,#12032,#12033,#12034,#12035,
#12036,#12037,#12038,#12039,#12040,#12041),.UNSPECIFIED.,.F.,.F.,(4,2,2,
2,2,2,2,2,2,2,4),(0.0464897534940957,0.0852567806515119,0.170513561303024,
0.246687263103517,0.308657850341199,0.370628437578881,0.432599024816563,
0.494569612054245,0.570743313854739,0.656000094506251,0.694767121663666),
 .UNSPECIFIED.);
#279=B_SPLINE_CURVE_WITH_KNOTS('',3,(#12045,#12046,#12047,#12048,#12049,
#12050,#12051,#12052,#12053,#12054,#12055,#12056),.UNSPECIFIED.,.F.,.F.,
(4,2,2,2,2,4),(0.0464897534940957,0.0852567806515119,0.170513561303024,
0.246687263103517,0.308657850341199,0.370628437578881),.UNSPECIFIED.);
#280=B_SPLINE_CURVE_WITH_KNOTS('',3,(#12061,#12062,#12063,#12064,#12065,
#12066,#12067,#12068,#12069,#12070,#12071,#12072),.UNSPECIFIED.,.F.,.F.,
(4,2,2,2,2,4),(0.370628437578881,0.432599024816563,0.494569612054245,0.570743313854738,
0.65600009450625,0.694767121663666),.UNSPECIFIED.);
#281=B_SPLINE_CURVE_WITH_KNOTS('',3,(#12076,#12077,#12078,#12079,#12080,
#12081,#12082,#12083,#12084,#12085,#12086,#12087,#12088,#12089,#12090,#12091,
#12092,#12093,#12094,#12095,#12096,#12097),.UNSPECIFIED.,.F.,.F.,(4,2,2,
2,2,2,2,2,2,2,4),(0.0464897534940957,0.0852567806515121,0.170513561303024,
0.246687263103518,0.308657850341199,0.370628437578881,0.432599024816563,
0.494569612054245,0.570743313854738,0.65600009450625,0.694767121663666),
 .UNSPECIFIED.);
#282=B_SPLINE_CURVE_WITH_KNOTS('',3,(#12101,#12102,#12103,#12104,#12105,
#12106,#12107,#12108,#12109,#12110,#12111,#12112,#12113,#12114,#12115,#12116,
#12117,#12118,#12119,#12120,#12121,#12122),.UNSPECIFIED.,.F.,.F.,(4,2,2,
2,2,2,2,2,2,2,4),(0.0464897534940957,0.0852567806515119,0.170513561303024,
0.246687263103517,0.308657850341199,0.370628437578881,0.432599024816563,
0.494569612054245,0.570743313854738,0.65600009450625,0.694767121663667),
 .UNSPECIFIED.);
#283=B_SPLINE_CURVE_WITH_KNOTS('',3,(#12126,#12127,#12128,#12129,#12130,
#12131,#12132,#12133,#12134,#12135,#12136,#12137,#12138,#12139,#12140,#12141,
#12142,#12143,#12144,#12145,#12146,#12147),.UNSPECIFIED.,.F.,.F.,(4,2,2,
2,2,2,2,2,2,2,4),(0.0464897534940957,0.0852567806515119,0.170513561303024,
0.246687263103517,0.308657850341199,0.370628437578881,0.432599024816563,
0.494569612054245,0.570743313854738,0.65600009450625,0.694767121663666),
 .UNSPECIFIED.);
#284=B_SPLINE_CURVE_WITH_KNOTS('',3,(#12151,#12152,#12153,#12154,#12155,
#12156,#12157,#12158,#12159,#12160,#12161,#12162,#12163,#12164,#12165,#12166,
#12167,#12168,#12169,#12170,#12171,#12172),.UNSPECIFIED.,.F.,.F.,(4,2,2,
2,2,2,2,2,2,2,4),(0.0464897534940957,0.0852567806515119,0.170513561303024,
0.246687263103517,0.308657850341199,0.370628437578881,0.432599024816563,
0.494569612054245,0.570743313854739,0.656000094506251,0.694767121663667),
 .UNSPECIFIED.);
#285=B_SPLINE_CURVE_WITH_KNOTS('',3,(#12180,#12181,#12182,#12183,#12184,
#12185,#12186,#12187,#12188,#12189,#12190,#12191,#12192,#12193,#12194,#12195,
#12196,#12197,#12198,#12199,#12200,#12201),.UNSPECIFIED.,.F.,.F.,(4,2,2,
2,2,2,2,2,2,2,4),(0.0473477652366656,0.126350602536658,0.189525903804987,
0.252701205073316,0.313298422430274,0.373895639787232,0.434492857144191,
0.495090074501149,0.558265375769478,0.621440677037807,0.7004435143378),
 .UNSPECIFIED.);
#286=B_SPLINE_CURVE_WITH_KNOTS('',3,(#12209,#12210,#12211,#12212,#12213,
#12214,#12215,#12216,#12217,#12218,#12219,#12220,#12221,#12222,#12223,#12224,
#12225,#12226,#12227,#12228,#12229,#12230),.UNSPECIFIED.,.F.,.F.,(4,2,2,
2,2,2,2,2,2,2,4),(0.0473477652366656,0.126350602536658,0.189525903804987,
0.252701205073317,0.313298422430275,0.373895639787233,0.434492857144191,
0.495090074501149,0.558265375769478,0.621440677037807,0.7004435143378),
 .UNSPECIFIED.);
#287=B_SPLINE_CURVE_WITH_KNOTS('',3,(#12239,#12240,#12241,#12242,#12243,
#12244,#12245,#12246,#12247,#12248,#12249,#12250),.UNSPECIFIED.,.F.,.F.,
(4,2,2,2,2,4),(0.0473477652366656,0.126350602536658,0.189525903804987,0.252701205073316,
0.313298422430275,0.373895639787233),.UNSPECIFIED.);
#288=B_SPLINE_CURVE_WITH_KNOTS('',3,(#12252,#12253,#12254,#12255,#12256,
#12257,#12258,#12259,#12260,#12261,#12262,#12263),.UNSPECIFIED.,.F.,.F.,
(4,2,2,2,2,4),(0.373895639787233,0.434492857144191,0.495090074501149,0.558265375769478,
0.621440677037807,0.7004435143378),.UNSPECIFIED.);
#289=B_SPLINE_CURVE_WITH_KNOTS('',3,(#12270,#12271,#12272,#12273,#12274,
#12275,#12276,#12277,#12278,#12279,#12280,#12281,#12282,#12283,#12284,#12285,
#12286,#12287,#12288,#12289,#12290,#12291),.UNSPECIFIED.,.F.,.F.,(4,2,2,
2,2,2,2,2,2,2,4),(0.0473477652366656,0.126350602536658,0.189525903804987,
0.252701205073316,0.313298422430275,0.373895639787233,0.434492857144191,
0.495090074501149,0.558265375769478,0.621440677037807,0.7004435143378),
 .UNSPECIFIED.);
#290=B_SPLINE_CURVE_WITH_KNOTS('',3,(#12299,#12300,#12301,#12302,#12303,
#12304,#12305,#12306,#12307,#12308,#12309,#12310,#12311,#12312,#12313,#12314,
#12315,#12316,#12317,#12318,#12319,#12320),.UNSPECIFIED.,.F.,.F.,(4,2,2,
2,2,2,2,2,2,2,4),(0.0473477652366656,0.126350602536658,0.189525903804987,
0.252701205073317,0.313298422430275,0.373895639787233,0.434492857144191,
0.495090074501149,0.558265375769478,0.621440677037807,0.7004435143378),
 .UNSPECIFIED.);
#291=B_SPLINE_CURVE_WITH_KNOTS('',3,(#12328,#12329,#12330,#12331,#12332,
#12333,#12334,#12335,#12336,#12337,#12338,#12339,#12340,#12341,#12342,#12343,
#12344,#12345,#12346,#12347,#12348,#12349),.UNSPECIFIED.,.F.,.F.,(4,2,2,
2,2,2,2,2,2,2,4),(0.0473477652366656,0.126350602536658,0.189525903804987,
0.252701205073316,0.313298422430275,0.373895639787233,0.434492857144191,
0.495090074501149,0.558265375769478,0.621440677037807,0.7004435143378),
 .UNSPECIFIED.);
#292=B_SPLINE_CURVE_WITH_KNOTS('',3,(#12358,#12359,#12360,#12361,#12362,
#12363,#12364,#12365,#12366,#12367,#12368,#12369,#12370,#12371,#12372,#12373,
#12374,#12375,#12376,#12377,#12378,#12379),.UNSPECIFIED.,.F.,.F.,(4,2,2,
2,2,2,2,2,2,2,4),(0.0473477652366656,0.126350602536658,0.189525903804987,
0.252701205073317,0.313298422430275,0.373895639787233,0.434492857144191,
0.495090074501149,0.558265375769478,0.621440677037807,0.7004435143378),
 .UNSPECIFIED.);
#319=SPHERICAL_SURFACE('',#7596,0.247676);
#320=SPHERICAL_SURFACE('',#7612,0.247676);
#321=SPHERICAL_SURFACE('',#7617,0.247676);
#322=SPHERICAL_SURFACE('',#7622,0.247676);
#323=SPHERICAL_SURFACE('',#7627,0.247676);
#324=SPHERICAL_SURFACE('',#7632,0.247676);
#325=SPHERICAL_SURFACE('',#7637,0.247676);
#326=SPHERICAL_SURFACE('',#7645,0.247676);
#378=SHAPE_REPRESENTATION_RELATIONSHIP('SRR','None',#12962,#415);
#415=ADVANCED_BREP_SHAPE_REPRESENTATION('',(#520),#12771);
#468=STYLED_ITEM('',(#13212),#520);
#520=MANIFOLD_SOLID_BREP('Continuous crown cage',#6539);
#626=FACE_BOUND('',#1691,.T.);
#825=PLANE('',#7609);
#826=PLANE('',#7614);
#827=PLANE('',#7619);
#828=PLANE('',#7624);
#829=PLANE('',#7629);
#830=PLANE('',#7634);
#831=PLANE('',#7643);
#832=PLANE('',#7647);
#833=PLANE('',#7648);
#1183=FACE_OUTER_BOUND('',#1673,.T.);
#1184=FACE_OUTER_BOUND('',#1674,.T.);
#1185=FACE_OUTER_BOUND('',#1675,.T.);
#1186=FACE_OUTER_BOUND('',#1676,.T.);
#1187=FACE_OUTER_BOUND('',#1677,.T.);
#1188=FACE_OUTER_BOUND('',#1678,.T.);
#1189=FACE_OUTER_BOUND('',#1679,.T.);
#1190=FACE_OUTER_BOUND('',#1680,.T.);
#1191=FACE_OUTER_BOUND('',#1681,.T.);
#1192=FACE_OUTER_BOUND('',#1682,.T.);
#1193=FACE_OUTER_BOUND('',#1683,.T.);
#1194=FACE_OUTER_BOUND('',#1684,.T.);
#1195=FACE_OUTER_BOUND('',#1685,.T.);
#1196=FACE_OUTER_BOUND('',#1686,.T.);
#1197=FACE_OUTER_BOUND('',#1687,.T.);
#1198=FACE_OUTER_BOUND('',#1688,.T.);
#1199=FACE_OUTER_BOUND('',#1689,.T.);
#1200=FACE_OUTER_BOUND('',#1690,.T.);
#1201=FACE_OUTER_BOUND('',#1692,.T.);
#1673=EDGE_LOOP('',(#5639,#5640,#5641,#5642));
#1674=EDGE_LOOP('',(#5643,#5644,#5645,#5646,#5647,#5648,#5649,#5650,#5651,
#5652,#5653,#5654,#5655,#5656,#5657,#5658,#5659,#5660,#5661,#5662));
#1675=EDGE_LOOP('',(#5663,#5664,#5665,#5666));
#1676=EDGE_LOOP('',(#5667,#5668,#5669,#5670));
#1677=EDGE_LOOP('',(#5671,#5672,#5673,#5674));
#1678=EDGE_LOOP('',(#5675,#5676,#5677,#5678));
#1679=EDGE_LOOP('',(#5679,#5680,#5681,#5682));
#1680=EDGE_LOOP('',(#5683,#5684,#5685,#5686,#5687,#5688));
#1681=EDGE_LOOP('',(#5689,#5690,#5691,#5692));
#1682=EDGE_LOOP('',(#5693,#5694,#5695,#5696));
#1683=EDGE_LOOP('',(#5697,#5698,#5699,#5700));
#1684=EDGE_LOOP('',(#5701,#5702,#5703,#5704));
#1685=EDGE_LOOP('',(#5705,#5706,#5707,#5708));
#1686=EDGE_LOOP('',(#5709,#5710,#5711,#5712));
#1687=EDGE_LOOP('',(#5713,#5714,#5715,#5716,#5717,#5718,#5719,#5720,#5721,
#5722,#5723,#5724,#5725,#5726,#5727,#5728,#5729,#5730,#5731,#5732));
#1688=EDGE_LOOP('',(#5733,#5734,#5735,#5736));
#1689=EDGE_LOOP('',(#5737,#5738,#5739,#5740));
#1690=EDGE_LOOP('',(#5741));
#1691=EDGE_LOOP('',(#5742));
#1692=EDGE_LOOP('',(#5743,#5744,#5745,#5746));
#2130=LINE('',#12058,#2545);
#2131=LINE('',#12354,#2546);
#2545=VECTOR('',#9440,1.019052);
#2546=VECTOR('',#9517,0.980948);
#2886=CIRCLE('',#7597,0.243053047864041);
#2887=CIRCLE('',#7598,0.243053047864041);
#2888=CIRCLE('',#7600,1.019052);
#2889=CIRCLE('',#7601,1.019052);
#2890=CIRCLE('',#7602,1.019052);
#2891=CIRCLE('',#7603,1.019052);
#2892=CIRCLE('',#7604,1.019052);
#2893=CIRCLE('',#7605,1.019052);
#2894=CIRCLE('',#7606,1.019052);
#2895=CIRCLE('',#7607,1.019052);
#2896=CIRCLE('',#7608,1.019052);
#2897=CIRCLE('',#7610,0.980948);
#2898=CIRCLE('',#7611,0.243053047864041);
#2899=CIRCLE('',#7613,0.243053047864041);
#2900=CIRCLE('',#7615,0.980948);
#2901=CIRCLE('',#7616,0.243053047864041);
#2902=CIRCLE('',#7618,0.243053047864041);
#2903=CIRCLE('',#7620,0.980948);
#2904=CIRCLE('',#7621,0.243053047864041);
#2905=CIRCLE('',#7623,0.243053047864041);
#2906=CIRCLE('',#7625,0.980948);
#2907=CIRCLE('',#7626,0.243053047864041);
#2908=CIRCLE('',#7628,0.243053047864041);
#2909=CIRCLE('',#7630,0.980948);
#2910=CIRCLE('',#7631,0.243053047864041);
#2911=CIRCLE('',#7633,0.243053047864041);
#2912=CIRCLE('',#7635,0.980948);
#2913=CIRCLE('',#7636,0.243053047864041);
#2914=CIRCLE('',#7638,0.243053047864041);
#2915=CIRCLE('',#7640,0.980948);
#2916=CIRCLE('',#7641,0.980948);
#2917=CIRCLE('',#7642,0.980948);
#2918=CIRCLE('',#7644,0.243053047864041);
#2919=CIRCLE('',#7646,0.243053047864041);
#3418=VERTEX_POINT('',#11941);
#3419=VERTEX_POINT('',#11942);
#3420=VERTEX_POINT('',#11965);
#3421=VERTEX_POINT('',#11967);
#3422=VERTEX_POINT('',#11992);
#3423=VERTEX_POINT('',#11994);
#3424=VERTEX_POINT('',#12017);
#3425=VERTEX_POINT('',#12019);
#3426=VERTEX_POINT('',#12042);
#3427=VERTEX_POINT('',#12044);
#3428=VERTEX_POINT('',#12057);
#3429=VERTEX_POINT('',#12060);
#3430=VERTEX_POINT('',#12073);
#3431=VERTEX_POINT('',#12075);
#3432=VERTEX_POINT('',#12098);
#3433=VERTEX_POINT('',#12100);
#3434=VERTEX_POINT('',#12123);
#3435=VERTEX_POINT('',#12125);
#3436=VERTEX_POINT('',#12148);
#3437=VERTEX_POINT('',#12150);
#3438=VERTEX_POINT('',#12175);
#3439=VERTEX_POINT('',#12179);
#3440=VERTEX_POINT('',#12204);
#3441=VERTEX_POINT('',#12208);
#3442=VERTEX_POINT('',#12233);
#3443=VERTEX_POINT('',#12237);
#3444=VERTEX_POINT('',#12238);
#3445=VERTEX_POINT('',#12265);
#3446=VERTEX_POINT('',#12269);
#3447=VERTEX_POINT('',#12294);
#3448=VERTEX_POINT('',#12298);
#3449=VERTEX_POINT('',#12323);
#3450=VERTEX_POINT('',#12327);
#3451=VERTEX_POINT('',#12352);
#3452=VERTEX_POINT('',#12355);
#3453=VERTEX_POINT('',#12357);
#4177=EDGE_CURVE('',#3418,#3419,#275,.T.);
#4178=EDGE_CURVE('',#3420,#3418,#2886,.T.);
#4179=EDGE_CURVE('',#3421,#3420,#276,.T.);
#4180=EDGE_CURVE('',#3419,#3421,#2887,.T.);
#4181=EDGE_CURVE('',#3422,#3420,#2888,.T.);
#4182=EDGE_CURVE('',#3422,#3423,#277,.T.);
#4183=EDGE_CURVE('',#3424,#3423,#2889,.T.);
#4184=EDGE_CURVE('',#3424,#3425,#278,.T.);
#4185=EDGE_CURVE('',#3426,#3425,#2890,.T.);
#4186=EDGE_CURVE('',#3426,#3427,#279,.T.);
#4187=EDGE_CURVE('',#3427,#3428,#2130,.T.);
#4188=EDGE_CURVE('',#3428,#3428,#2891,.T.);
#4189=EDGE_CURVE('',#3427,#3429,#280,.T.);
#4190=EDGE_CURVE('',#3430,#3429,#2892,.T.);
#4191=EDGE_CURVE('',#3430,#3431,#281,.T.);
#4192=EDGE_CURVE('',#3432,#3431,#2893,.T.);
#4193=EDGE_CURVE('',#3432,#3433,#282,.T.);
#4194=EDGE_CURVE('',#3434,#3433,#2894,.T.);
#4195=EDGE_CURVE('',#3434,#3435,#283,.T.);
#4196=EDGE_CURVE('',#3436,#3435,#2895,.T.);
#4197=EDGE_CURVE('',#3436,#3437,#284,.T.);
#4198=EDGE_CURVE('',#3421,#3437,#2896,.T.);
#4199=EDGE_CURVE('',#3418,#3438,#2897,.T.);
#4200=EDGE_CURVE('',#3438,#3422,#2898,.T.);
#4201=EDGE_CURVE('',#3439,#3438,#285,.T.);
#4202=EDGE_CURVE('',#3423,#3439,#2899,.T.);
#4203=EDGE_CURVE('',#3439,#3440,#2900,.T.);
#4204=EDGE_CURVE('',#3440,#3424,#2901,.T.);
#4205=EDGE_CURVE('',#3441,#3440,#286,.T.);
#4206=EDGE_CURVE('',#3425,#3441,#2902,.T.);
#4207=EDGE_CURVE('',#3441,#3442,#2903,.T.);
#4208=EDGE_CURVE('',#3442,#3426,#2904,.T.);
#4209=EDGE_CURVE('',#3443,#3444,#287,.T.);
#4210=EDGE_CURVE('',#3429,#3443,#2905,.T.);
#4211=EDGE_CURVE('',#3444,#3442,#288,.T.);
#4212=EDGE_CURVE('',#3443,#3445,#2906,.T.);
#4213=EDGE_CURVE('',#3445,#3430,#2907,.T.);
#4214=EDGE_CURVE('',#3446,#3445,#289,.T.);
#4215=EDGE_CURVE('',#3431,#3446,#2908,.T.);
#4216=EDGE_CURVE('',#3446,#3447,#2909,.T.);
#4217=EDGE_CURVE('',#3447,#3432,#2910,.T.);
#4218=EDGE_CURVE('',#3448,#3447,#290,.T.);
#4219=EDGE_CURVE('',#3433,#3448,#2911,.T.);
#4220=EDGE_CURVE('',#3448,#3449,#2912,.T.);
#4221=EDGE_CURVE('',#3449,#3434,#2913,.T.);
#4222=EDGE_CURVE('',#3450,#3449,#291,.T.);
#4223=EDGE_CURVE('',#3435,#3450,#2914,.T.);
#4224=EDGE_CURVE('',#3451,#3451,#2915,.T.);
#4225=EDGE_CURVE('',#3451,#3444,#2131,.T.);
#4226=EDGE_CURVE('',#3452,#3419,#2916,.T.);
#4227=EDGE_CURVE('',#3452,#3453,#292,.T.);
#4228=EDGE_CURVE('',#3450,#3453,#2917,.T.);
#4229=EDGE_CURVE('',#3437,#3452,#2918,.T.);
#4230=EDGE_CURVE('',#3453,#3436,#2919,.T.);
#5639=ORIENTED_EDGE('',*,*,#4177,.F.);
#5640=ORIENTED_EDGE('',*,*,#4178,.F.);
#5641=ORIENTED_EDGE('',*,*,#4179,.F.);
#5642=ORIENTED_EDGE('',*,*,#4180,.F.);
#5643=ORIENTED_EDGE('',*,*,#4179,.T.);
#5644=ORIENTED_EDGE('',*,*,#4181,.F.);
#5645=ORIENTED_EDGE('',*,*,#4182,.T.);
#5646=ORIENTED_EDGE('',*,*,#4183,.F.);
#5647=ORIENTED_EDGE('',*,*,#4184,.T.);
#5648=ORIENTED_EDGE('',*,*,#4185,.F.);
#5649=ORIENTED_EDGE('',*,*,#4186,.T.);
#5650=ORIENTED_EDGE('',*,*,#4187,.T.);
#5651=ORIENTED_EDGE('',*,*,#4188,.F.);
#5652=ORIENTED_EDGE('',*,*,#4187,.F.);
#5653=ORIENTED_EDGE('',*,*,#4189,.T.);
#5654=ORIENTED_EDGE('',*,*,#4190,.F.);
#5655=ORIENTED_EDGE('',*,*,#4191,.T.);
#5656=ORIENTED_EDGE('',*,*,#4192,.F.);
#5657=ORIENTED_EDGE('',*,*,#4193,.T.);
#5658=ORIENTED_EDGE('',*,*,#4194,.F.);
#5659=ORIENTED_EDGE('',*,*,#4195,.T.);
#5660=ORIENTED_EDGE('',*,*,#4196,.F.);
#5661=ORIENTED_EDGE('',*,*,#4197,.T.);
#5662=ORIENTED_EDGE('',*,*,#4198,.F.);
#5663=ORIENTED_EDGE('',*,*,#4178,.T.);
#5664=ORIENTED_EDGE('',*,*,#4199,.T.);
#5665=ORIENTED_EDGE('',*,*,#4200,.T.);
#5666=ORIENTED_EDGE('',*,*,#4181,.T.);
#5667=ORIENTED_EDGE('',*,*,#4201,.F.);
#5668=ORIENTED_EDGE('',*,*,#4202,.F.);
#5669=ORIENTED_EDGE('',*,*,#4182,.F.);
#5670=ORIENTED_EDGE('',*,*,#4200,.F.);
#5671=ORIENTED_EDGE('',*,*,#4202,.T.);
#5672=ORIENTED_EDGE('',*,*,#4203,.T.);
#5673=ORIENTED_EDGE('',*,*,#4204,.T.);
#5674=ORIENTED_EDGE('',*,*,#4183,.T.);
#5675=ORIENTED_EDGE('',*,*,#4205,.F.);
#5676=ORIENTED_EDGE('',*,*,#4206,.F.);
#5677=ORIENTED_EDGE('',*,*,#4184,.F.);
#5678=ORIENTED_EDGE('',*,*,#4204,.F.);
#5679=ORIENTED_EDGE('',*,*,#4206,.T.);
#5680=ORIENTED_EDGE('',*,*,#4207,.T.);
#5681=ORIENTED_EDGE('',*,*,#4208,.T.);
#5682=ORIENTED_EDGE('',*,*,#4185,.T.);
#5683=ORIENTED_EDGE('',*,*,#4209,.F.);
#5684=ORIENTED_EDGE('',*,*,#4210,.F.);
#5685=ORIENTED_EDGE('',*,*,#4189,.F.);
#5686=ORIENTED_EDGE('',*,*,#4186,.F.);
#5687=ORIENTED_EDGE('',*,*,#4208,.F.);
#5688=ORIENTED_EDGE('',*,*,#4211,.F.);
#5689=ORIENTED_EDGE('',*,*,#4210,.T.);
#5690=ORIENTED_EDGE('',*,*,#4212,.T.);
#5691=ORIENTED_EDGE('',*,*,#4213,.T.);
#5692=ORIENTED_EDGE('',*,*,#4190,.T.);
#5693=ORIENTED_EDGE('',*,*,#4214,.F.);
#5694=ORIENTED_EDGE('',*,*,#4215,.F.);
#5695=ORIENTED_EDGE('',*,*,#4191,.F.);
#5696=ORIENTED_EDGE('',*,*,#4213,.F.);
#5697=ORIENTED_EDGE('',*,*,#4215,.T.);
#5698=ORIENTED_EDGE('',*,*,#4216,.T.);
#5699=ORIENTED_EDGE('',*,*,#4217,.T.);
#5700=ORIENTED_EDGE('',*,*,#4192,.T.);
#5701=ORIENTED_EDGE('',*,*,#4218,.F.);
#5702=ORIENTED_EDGE('',*,*,#4219,.F.);
#5703=ORIENTED_EDGE('',*,*,#4193,.F.);
#5704=ORIENTED_EDGE('',*,*,#4217,.F.);
#5705=ORIENTED_EDGE('',*,*,#4219,.T.);
#5706=ORIENTED_EDGE('',*,*,#4220,.T.);
#5707=ORIENTED_EDGE('',*,*,#4221,.T.);
#5708=ORIENTED_EDGE('',*,*,#4194,.T.);
#5709=ORIENTED_EDGE('',*,*,#4195,.F.);
#5710=ORIENTED_EDGE('',*,*,#4221,.F.);
#5711=ORIENTED_EDGE('',*,*,#4222,.F.);
#5712=ORIENTED_EDGE('',*,*,#4223,.F.);
#5713=ORIENTED_EDGE('',*,*,#4224,.F.);
#5714=ORIENTED_EDGE('',*,*,#4225,.T.);
#5715=ORIENTED_EDGE('',*,*,#4211,.T.);
#5716=ORIENTED_EDGE('',*,*,#4207,.F.);
#5717=ORIENTED_EDGE('',*,*,#4205,.T.);
#5718=ORIENTED_EDGE('',*,*,#4203,.F.);
#5719=ORIENTED_EDGE('',*,*,#4201,.T.);
#5720=ORIENTED_EDGE('',*,*,#4199,.F.);
#5721=ORIENTED_EDGE('',*,*,#4177,.T.);
#5722=ORIENTED_EDGE('',*,*,#4226,.F.);
#5723=ORIENTED_EDGE('',*,*,#4227,.T.);
#5724=ORIENTED_EDGE('',*,*,#4228,.F.);
#5725=ORIENTED_EDGE('',*,*,#4222,.T.);
#5726=ORIENTED_EDGE('',*,*,#4220,.F.);
#5727=ORIENTED_EDGE('',*,*,#4218,.T.);
#5728=ORIENTED_EDGE('',*,*,#4216,.F.);
#5729=ORIENTED_EDGE('',*,*,#4214,.T.);
#5730=ORIENTED_EDGE('',*,*,#4212,.F.);
#5731=ORIENTED_EDGE('',*,*,#4209,.T.);
#5732=ORIENTED_EDGE('',*,*,#4225,.F.);
#5733=ORIENTED_EDGE('',*,*,#4180,.T.);
#5734=ORIENTED_EDGE('',*,*,#4198,.T.);
#5735=ORIENTED_EDGE('',*,*,#4229,.T.);
#5736=ORIENTED_EDGE('',*,*,#4226,.T.);
#5737=ORIENTED_EDGE('',*,*,#4197,.F.);
#5738=ORIENTED_EDGE('',*,*,#4230,.F.);
#5739=ORIENTED_EDGE('',*,*,#4227,.F.);
#5740=ORIENTED_EDGE('',*,*,#4229,.F.);
#5741=ORIENTED_EDGE('',*,*,#4188,.T.);
#5742=ORIENTED_EDGE('',*,*,#4224,.T.);
#5743=ORIENTED_EDGE('',*,*,#4223,.T.);
#5744=ORIENTED_EDGE('',*,*,#4228,.T.);
#5745=ORIENTED_EDGE('',*,*,#4230,.T.);
#5746=ORIENTED_EDGE('',*,*,#4196,.T.);
#6074=CYLINDRICAL_SURFACE('',#7599,1.019052);
#6075=CYLINDRICAL_SURFACE('',#7639,0.980948);
#6408=ADVANCED_FACE('',(#1183),#319,.F.);
#6409=ADVANCED_FACE('',(#1184),#6074,.T.);
#6410=ADVANCED_FACE('',(#1185),#825,.T.);
#6411=ADVANCED_FACE('',(#1186),#320,.F.);
#6412=ADVANCED_FACE('',(#1187),#826,.T.);
#6413=ADVANCED_FACE('',(#1188),#321,.F.);
#6414=ADVANCED_FACE('',(#1189),#827,.T.);
#6415=ADVANCED_FACE('',(#1190),#322,.F.);
#6416=ADVANCED_FACE('',(#1191),#828,.T.);
#6417=ADVANCED_FACE('',(#1192),#323,.F.);
#6418=ADVANCED_FACE('',(#1193),#829,.T.);
#6419=ADVANCED_FACE('',(#1194),#324,.F.);
#6420=ADVANCED_FACE('',(#1195),#830,.T.);
#6421=ADVANCED_FACE('',(#1196),#325,.F.);
#6422=ADVANCED_FACE('',(#1197),#6075,.F.);
#6423=ADVANCED_FACE('',(#1198),#831,.T.);
#6424=ADVANCED_FACE('',(#1199),#326,.F.);
#6425=ADVANCED_FACE('',(#1200,#626),#832,.T.);
#6426=ADVANCED_FACE('',(#1201),#833,.T.);
#6539=CLOSED_SHELL('',(#6408,#6409,#6410,#6411,#6412,#6413,#6414,#6415,
#6416,#6417,#6418,#6419,#6420,#6421,#6422,#6423,#6424,#6425,#6426));
#7595=AXIS2_PLACEMENT_3D('',#11939,#9424,#9425);
#7596=AXIS2_PLACEMENT_3D('',#11940,#9426,#9427);
#7597=AXIS2_PLACEMENT_3D('',#11966,#9428,#9429);
#7598=AXIS2_PLACEMENT_3D('',#11990,#9430,#9431);
#7599=AXIS2_PLACEMENT_3D('',#11991,#9432,#9433);
#7600=AXIS2_PLACEMENT_3D('',#11993,#9434,#9435);
#7601=AXIS2_PLACEMENT_3D('',#12018,#9436,#9437);
#7602=AXIS2_PLACEMENT_3D('',#12043,#9438,#9439);
#7603=AXIS2_PLACEMENT_3D('',#12059,#9441,#9442);
#7604=AXIS2_PLACEMENT_3D('',#12074,#9443,#9444);
#7605=AXIS2_PLACEMENT_3D('',#12099,#9445,#9446);
#7606=AXIS2_PLACEMENT_3D('',#12124,#9447,#9448);
#7607=AXIS2_PLACEMENT_3D('',#12149,#9449,#9450);
#7608=AXIS2_PLACEMENT_3D('',#12173,#9451,#9452);
#7609=AXIS2_PLACEMENT_3D('',#12174,#9453,#9454);
#7610=AXIS2_PLACEMENT_3D('',#12176,#9455,#9456);
#7611=AXIS2_PLACEMENT_3D('',#12177,#9457,#9458);
#7612=AXIS2_PLACEMENT_3D('',#12178,#9459,#9460);
#7613=AXIS2_PLACEMENT_3D('',#12202,#9461,#9462);
#7614=AXIS2_PLACEMENT_3D('',#12203,#9463,#9464);
#7615=AXIS2_PLACEMENT_3D('',#12205,#9465,#9466);
#7616=AXIS2_PLACEMENT_3D('',#12206,#9467,#9468);
#7617=AXIS2_PLACEMENT_3D('',#12207,#9469,#9470);
#7618=AXIS2_PLACEMENT_3D('',#12231,#9471,#9472);
#7619=AXIS2_PLACEMENT_3D('',#12232,#9473,#9474);
#7620=AXIS2_PLACEMENT_3D('',#12234,#9475,#9476);
#7621=AXIS2_PLACEMENT_3D('',#12235,#9477,#9478);
#7622=AXIS2_PLACEMENT_3D('',#12236,#9479,#9480);
#7623=AXIS2_PLACEMENT_3D('',#12251,#9481,#9482);
#7624=AXIS2_PLACEMENT_3D('',#12264,#9483,#9484);
#7625=AXIS2_PLACEMENT_3D('',#12266,#9485,#9486);
#7626=AXIS2_PLACEMENT_3D('',#12267,#9487,#9488);
#7627=AXIS2_PLACEMENT_3D('',#12268,#9489,#9490);
#7628=AXIS2_PLACEMENT_3D('',#12292,#9491,#9492);
#7629=AXIS2_PLACEMENT_3D('',#12293,#9493,#9494);
#7630=AXIS2_PLACEMENT_3D('',#12295,#9495,#9496);
#7631=AXIS2_PLACEMENT_3D('',#12296,#9497,#9498);
#7632=AXIS2_PLACEMENT_3D('',#12297,#9499,#9500);
#7633=AXIS2_PLACEMENT_3D('',#12321,#9501,#9502);
#7634=AXIS2_PLACEMENT_3D('',#12322,#9503,#9504);
#7635=AXIS2_PLACEMENT_3D('',#12324,#9505,#9506);
#7636=AXIS2_PLACEMENT_3D('',#12325,#9507,#9508);
#7637=AXIS2_PLACEMENT_3D('',#12326,#9509,#9510);
#7638=AXIS2_PLACEMENT_3D('',#12350,#9511,#9512);
#7639=AXIS2_PLACEMENT_3D('',#12351,#9513,#9514);
#7640=AXIS2_PLACEMENT_3D('',#12353,#9515,#9516);
#7641=AXIS2_PLACEMENT_3D('',#12356,#9518,#9519);
#7642=AXIS2_PLACEMENT_3D('',#12380,#9520,#9521);
#7643=AXIS2_PLACEMENT_3D('',#12381,#9522,#9523);
#7644=AXIS2_PLACEMENT_3D('',#12382,#9524,#9525);
#7645=AXIS2_PLACEMENT_3D('',#12383,#9526,#9527);
#7646=AXIS2_PLACEMENT_3D('',#12384,#9528,#9529);
#7647=AXIS2_PLACEMENT_3D('',#12385,#9530,#9531);
#7648=AXIS2_PLACEMENT_3D('',#12386,#9532,#9533);
#9424=DIRECTION('axis',(0.,0.,1.));
#9425=DIRECTION('refdir',(1.,0.,0.));
#9426=DIRECTION('center_axis',(0.,0.,1.));
#9427=DIRECTION('ref_axis',(1.,0.,0.));
#9428=DIRECTION('center_axis',(0.,-1.,0.));
#9429=DIRECTION('ref_axis',(0.,0.,-1.));
#9430=DIRECTION('center_axis',(0.,-1.,0.));
#9431=DIRECTION('ref_axis',(0.,0.,-1.));
#9432=DIRECTION('center_axis',(0.,1.,0.));
#9433=DIRECTION('ref_axis',(1.,0.,0.));
#9434=DIRECTION('center_axis',(0.,1.,0.));
#9435=DIRECTION('ref_axis',(1.,0.,0.));
#9436=DIRECTION('center_axis',(0.,1.,0.));
#9437=DIRECTION('ref_axis',(1.,0.,0.));
#9438=DIRECTION('center_axis',(0.,1.,0.));
#9439=DIRECTION('ref_axis',(1.,0.,0.));
#9440=DIRECTION('',(0.,-1.,0.));
#9441=DIRECTION('center_axis',(0.,-1.,0.));
#9442=DIRECTION('ref_axis',(1.,0.,0.));
#9443=DIRECTION('center_axis',(0.,1.,0.));
#9444=DIRECTION('ref_axis',(1.,0.,0.));
#9445=DIRECTION('center_axis',(0.,1.,0.));
#9446=DIRECTION('ref_axis',(1.,0.,0.));
#9447=DIRECTION('center_axis',(0.,1.,0.));
#9448=DIRECTION('ref_axis',(1.,0.,0.));
#9449=DIRECTION('center_axis',(0.,1.,0.));
#9450=DIRECTION('ref_axis',(1.,0.,0.));
#9451=DIRECTION('center_axis',(0.,1.,0.));
#9452=DIRECTION('ref_axis',(1.,0.,0.));
#9453=DIRECTION('center_axis',(0.,1.,0.));
#9454=DIRECTION('ref_axis',(1.,0.,0.));
#9455=DIRECTION('center_axis',(0.,-1.,0.));
#9456=DIRECTION('ref_axis',(1.,0.,0.));
#9457=DIRECTION('center_axis',(0.,-1.,0.));
#9458=DIRECTION('ref_axis',(0.,0.,-1.));
#9459=DIRECTION('center_axis',(6.12323399573677E-17,0.,1.));
#9460=DIRECTION('ref_axis',(1.,0.,0.));
#9461=DIRECTION('center_axis',(0.,-1.,0.));
#9462=DIRECTION('ref_axis',(0.,0.,-1.));
#9463=DIRECTION('center_axis',(0.,1.,0.));
#9464=DIRECTION('ref_axis',(1.,0.,0.));
#9465=DIRECTION('center_axis',(0.,-1.,0.));
#9466=DIRECTION('ref_axis',(1.,0.,0.));
#9467=DIRECTION('center_axis',(0.,-1.,0.));
#9468=DIRECTION('ref_axis',(0.,0.,-1.));
#9469=DIRECTION('center_axis',(0.,0.,1.));
#9470=DIRECTION('ref_axis',(1.,0.,0.));
#9471=DIRECTION('center_axis',(0.,-1.,0.));
#9472=DIRECTION('ref_axis',(0.,0.,-1.));
#9473=DIRECTION('center_axis',(0.,1.,0.));
#9474=DIRECTION('ref_axis',(1.,0.,0.));
#9475=DIRECTION('center_axis',(0.,-1.,0.));
#9476=DIRECTION('ref_axis',(1.,0.,0.));
#9477=DIRECTION('center_axis',(0.,-1.,0.));
#9478=DIRECTION('ref_axis',(0.,0.,-1.));
#9479=DIRECTION('center_axis',(0.,0.,1.));
#9480=DIRECTION('ref_axis',(1.,0.,0.));
#9481=DIRECTION('center_axis',(0.,-1.,0.));
#9482=DIRECTION('ref_axis',(0.,0.,-1.));
#9483=DIRECTION('center_axis',(0.,1.,0.));
#9484=DIRECTION('ref_axis',(1.,0.,0.));
#9485=DIRECTION('center_axis',(0.,-1.,0.));
#9486=DIRECTION('ref_axis',(1.,0.,0.));
#9487=DIRECTION('center_axis',(0.,-1.,0.));
#9488=DIRECTION('ref_axis',(0.,0.,-1.));
#9489=DIRECTION('center_axis',(0.,0.,1.));
#9490=DIRECTION('ref_axis',(1.,0.,0.));
#9491=DIRECTION('center_axis',(0.,-1.,0.));
#9492=DIRECTION('ref_axis',(0.,0.,-1.));
#9493=DIRECTION('center_axis',(0.,1.,0.));
#9494=DIRECTION('ref_axis',(1.,0.,0.));
#9495=DIRECTION('center_axis',(0.,-1.,0.));
#9496=DIRECTION('ref_axis',(1.,0.,0.));
#9497=DIRECTION('center_axis',(0.,-1.,0.));
#9498=DIRECTION('ref_axis',(0.,0.,-1.));
#9499=DIRECTION('center_axis',(6.12323399573676E-17,0.,1.));
#9500=DIRECTION('ref_axis',(1.,0.,0.));
#9501=DIRECTION('center_axis',(0.,-1.,0.));
#9502=DIRECTION('ref_axis',(0.,0.,-1.));
#9503=DIRECTION('center_axis',(0.,1.,0.));
#9504=DIRECTION('ref_axis',(1.,0.,0.));
#9505=DIRECTION('center_axis',(0.,-1.,0.));
#9506=DIRECTION('ref_axis',(1.,0.,0.));
#9507=DIRECTION('center_axis',(0.,-1.,0.));
#9508=DIRECTION('ref_axis',(0.,0.,-1.));
#9509=DIRECTION('center_axis',(0.,0.,1.));
#9510=DIRECTION('ref_axis',(1.,0.,0.));
#9511=DIRECTION('center_axis',(0.,-1.,0.));
#9512=DIRECTION('ref_axis',(0.,0.,-1.));
#9513=DIRECTION('center_axis',(0.,1.,0.));
#9514=DIRECTION('ref_axis',(1.,0.,0.));
#9515=DIRECTION('center_axis',(0.,1.,0.));
#9516=DIRECTION('ref_axis',(1.,0.,0.));
#9517=DIRECTION('',(0.,1.,0.));
#9518=DIRECTION('center_axis',(0.,-1.,0.));
#9519=DIRECTION('ref_axis',(1.,0.,0.));
#9520=DIRECTION('center_axis',(0.,-1.,0.));
#9521=DIRECTION('ref_axis',(1.,0.,0.));
#9522=DIRECTION('center_axis',(0.,1.,0.));
#9523=DIRECTION('ref_axis',(1.,0.,0.));
#9524=DIRECTION('center_axis',(0.,-1.,0.));
#9525=DIRECTION('ref_axis',(0.,0.,-1.));
#9526=DIRECTION('center_axis',(0.,0.,1.));
#9527=DIRECTION('ref_axis',(1.,0.,0.));
#9528=DIRECTION('center_axis',(0.,-1.,0.));
#9529=DIRECTION('ref_axis',(0.,0.,-1.));
#9530=DIRECTION('center_axis',(0.,-1.,0.));
#9531=DIRECTION('ref_axis',(-1.,0.,0.));
#9532=DIRECTION('center_axis',(0.,1.,0.));
#9533=DIRECTION('ref_axis',(1.,0.,0.));
#11939=CARTESIAN_POINT('',(0.,0.,0.));
#11940=CARTESIAN_POINT('Origin',(0.707106781186547,0.,0.707106781186548));
#11941=CARTESIAN_POINT('',(0.504455939115715,-0.04763,0.841298510752802));
#11942=CARTESIAN_POINT('',(0.841298510752802,-0.04763,0.504455939115715));
#11943=CARTESIAN_POINT('Ctrl Pts',(0.504455939115715,-0.04763,0.841298510752802));
#11944=CARTESIAN_POINT('Ctrl Pts',(0.508899795931835,-0.0740444353928835,
0.838633903678357));
#11945=CARTESIAN_POINT('Ctrl Pts',(0.517157748491652,-0.0999305678883309,
0.833661031856294));
#11946=CARTESIAN_POINT('Ctrl Pts',(0.537715343527944,-0.142345102874864,
0.820511285096538));
#11947=CARTESIAN_POINT('Ctrl Pts',(0.548874290046456,-0.159766064500479,
0.813159949759));
#11948=CARTESIAN_POINT('Ctrl Pts',(0.573915184558107,-0.190326085855194,
0.795684265985089));
#11949=CARTESIAN_POINT('Ctrl Pts',(0.587792702767295,-0.203463743702801,
0.78555112003688));
#11950=CARTESIAN_POINT('Ctrl Pts',(0.615966552324775,-0.224161999508995,
0.763642258217233));
#11951=CARTESIAN_POINT('Ctrl Pts',(0.631684198665438,-0.232861760990032,
0.750785745543687));
#11952=CARTESIAN_POINT('Ctrl Pts',(0.663382628119203,-0.244251601209411,
0.722929908501543));
#11953=CARTESIAN_POINT('Ctrl Pts',(0.679352081686668,-0.246942143572133,
0.707917883896095));
#11954=CARTESIAN_POINT('Ctrl Pts',(0.707917883896095,-0.246942143572133,
0.679352081686668));
#11955=CARTESIAN_POINT('Ctrl Pts',(0.722929908501543,-0.244251601209411,
0.663382628119203));
#11956=CARTESIAN_POINT('Ctrl Pts',(0.750785745543687,-0.232861760990032,
0.631684198665439));
#11957=CARTESIAN_POINT('Ctrl Pts',(0.763642258217232,-0.224161999508995,
0.615966552324775));
#11958=CARTESIAN_POINT('Ctrl Pts',(0.78555112003688,-0.203463743702801,
0.587792702767295));
#11959=CARTESIAN_POINT('Ctrl Pts',(0.795684265985088,-0.190326085855194,
0.573915184558108));
#11960=CARTESIAN_POINT('Ctrl Pts',(0.813159949759,-0.15976606450048,0.548874290046456));
#11961=CARTESIAN_POINT('Ctrl Pts',(0.820511285096538,-0.142345102874864,
0.537715343527944));
#11962=CARTESIAN_POINT('Ctrl Pts',(0.833661031856294,-0.099930567888331,
0.517157748491653));
#11963=CARTESIAN_POINT('Ctrl Pts',(0.838633903678357,-0.0740444353928835,
0.508899795931835));
#11964=CARTESIAN_POINT('Ctrl Pts',(0.841298510752801,-0.0476299999999999,
0.504455939115715));
#11965=CARTESIAN_POINT('',(0.528110872004958,-0.04763,0.871530771444223));
#11966=CARTESIAN_POINT('Origin',(0.707106781186547,-0.04763,0.707106781186548));
#11967=CARTESIAN_POINT('',(0.871530771444223,-0.04763,0.528110872004959));
#11968=CARTESIAN_POINT('Ctrl Pts',(0.871530771444223,-0.0476300000000001,
0.528110872004958));
#11969=CARTESIAN_POINT('Ctrl Pts',(0.87014664509073,-0.0609922781173483,
0.530395067942936));
#11970=CARTESIAN_POINT('Ctrl Pts',(0.868149331745851,-0.0742967091364493,
0.533674141594226));
#11971=CARTESIAN_POINT('Ctrl Pts',(0.85981294420286,-0.115492077056649,
0.54708917182331));
#11972=CARTESIAN_POINT('Ctrl Pts',(0.850993704737257,-0.141695629206859,
0.560922177770136));
#11973=CARTESIAN_POINT('Ctrl Pts',(0.830754510485543,-0.181890537957859,
0.590422647829571));
#11974=CARTESIAN_POINT('Ctrl Pts',(0.816896541396381,-0.201072148666545,
0.609616703125488));
#11975=CARTESIAN_POINT('Ctrl Pts',(0.792310597819928,-0.223955109275652,
0.641117951819998));
#11976=CARTESIAN_POINT('Ctrl Pts',(0.779109323683612,-0.232742381310829,
0.657208095763053));
#11977=CARTESIAN_POINT('Ctrl Pts',(0.750552691816206,-0.244234834628584,
0.68964083160521));
#11978=CARTESIAN_POINT('Ctrl Pts',(0.735185187071673,-0.246942143572133,
0.705971972091755));
#11979=CARTESIAN_POINT('Ctrl Pts',(0.705971972091754,-0.246942143572133,
0.735185187071673));
#11980=CARTESIAN_POINT('Ctrl Pts',(0.689640831605209,-0.244234834628584,
0.750552691816206));
#11981=CARTESIAN_POINT('Ctrl Pts',(0.657208095763052,-0.232742381310829,
0.779109323683612));
#11982=CARTESIAN_POINT('Ctrl Pts',(0.641117951819998,-0.223955109275652,
0.792310597819928));
#11983=CARTESIAN_POINT('Ctrl Pts',(0.609616703125487,-0.201072148666545,
0.816896541396382));
#11984=CARTESIAN_POINT('Ctrl Pts',(0.590422647829571,-0.181890537957858,
0.830754510485544));
#11985=CARTESIAN_POINT('Ctrl Pts',(0.560922177770135,-0.141695629206858,
0.850993704737257));
#11986=CARTESIAN_POINT('Ctrl Pts',(0.547089171823309,-0.115492077056649,
0.859812944202861));
#11987=CARTESIAN_POINT('Ctrl Pts',(0.533674141594226,-0.0742967091364491,
0.868149331745852));
#11988=CARTESIAN_POINT('Ctrl Pts',(0.530395067942936,-0.0609922781173483,
0.870146645090731));
#11989=CARTESIAN_POINT('Ctrl Pts',(0.528110872004958,-0.0476300000000001,
0.871530771444223));
#11990=CARTESIAN_POINT('Origin',(0.707106781186547,-0.04763,0.707106781186548));
#11991=CARTESIAN_POINT('Origin',(0.,-0.166705,0.));
#11992=CARTESIAN_POINT('',(0.242834539687906,-0.04763,0.989696097314));
#11993=CARTESIAN_POINT('Origin',(0.,-0.04763,0.));
#11994=CARTESIAN_POINT('',(-0.242834539687907,-0.04763,0.989696097314));
#11995=CARTESIAN_POINT('Ctrl Pts',(0.242834539687906,-0.04763,0.989696097314));
#11996=CARTESIAN_POINT('Ctrl Pts',(0.24024064412003,-0.0609922781173483,
0.990332542620729));
#11997=CARTESIAN_POINT('Ctrl Pts',(0.236509675094874,-0.0742967091364492,
0.991238884025248));
#11998=CARTESIAN_POINT('Ctrl Pts',(0.221129100087819,-0.115492077056649,
0.994830026707808));
#11999=CARTESIAN_POINT('Ctrl Pts',(0.205111543747588,-0.141695629206859,
0.998375294985966));
#12000=CARTESIAN_POINT('Ctrl Pts',(0.169940289819232,-0.181890537957859,
1.00492400591205));
#12001=CARTESIAN_POINT('Ctrl Pts',(0.1465689792446,-0.201072148666545,1.00869718865384));
#12002=CARTESIAN_POINT('Ctrl Pts',(0.106909345252087,-0.223955109275652,
1.01358704779679));
#12003=CARTESIAN_POINT('Ctrl Pts',(0.0861971848975941,-0.232742381310829,
1.0156297872271));
#12004=CARTESIAN_POINT('Ctrl Pts',(0.0430711894098822,-0.244234834628584,
1.01837060663223));
#12005=CARTESIAN_POINT('Ctrl Pts',(0.0206568624125605,-0.246942143572133,
1.019052));
#12006=CARTESIAN_POINT('Ctrl Pts',(-0.0206568624125608,-0.246942143572133,
1.019052));
#12007=CARTESIAN_POINT('Ctrl Pts',(-0.0430711894098825,-0.244234834628584,
1.01837060663223));
#12008=CARTESIAN_POINT('Ctrl Pts',(-0.0861971848975943,-0.232742381310829,
1.0156297872271));
#12009=CARTESIAN_POINT('Ctrl Pts',(-0.106909345252088,-0.223955109275652,
1.01358704779679));
#12010=CARTESIAN_POINT('Ctrl Pts',(-0.1465689792446,-0.201072148666545,
1.00869718865384));
#12011=CARTESIAN_POINT('Ctrl Pts',(-0.169940289819232,-0.181890537957859,
1.00492400591205));
#12012=CARTESIAN_POINT('Ctrl Pts',(-0.205111543747588,-0.141695629206859,
0.998375294985966));
#12013=CARTESIAN_POINT('Ctrl Pts',(-0.221129100087819,-0.115492077056649,
0.994830026707808));
#12014=CARTESIAN_POINT('Ctrl Pts',(-0.236509675094875,-0.0742967091364493,
0.991238884025248));
#12015=CARTESIAN_POINT('Ctrl Pts',(-0.24024064412003,-0.0609922781173483,
0.990332542620729));
#12016=CARTESIAN_POINT('Ctrl Pts',(-0.242834539687907,-0.04763,0.989696097314));
#12017=CARTESIAN_POINT('',(-0.528110872004959,-0.04763,0.871530771444223));
#12018=CARTESIAN_POINT('Origin',(0.,-0.04763,0.));
#12019=CARTESIAN_POINT('',(-0.871530771444223,-0.04763,0.528110872004958));
#12020=CARTESIAN_POINT('Ctrl Pts',(-0.528110872004958,-0.0476300000000001,
0.871530771444223));
#12021=CARTESIAN_POINT('Ctrl Pts',(-0.530395067942936,-0.0609922781173484,
0.87014664509073));
#12022=CARTESIAN_POINT('Ctrl Pts',(-0.533674141594226,-0.0742967091364493,
0.868149331745851));
#12023=CARTESIAN_POINT('Ctrl Pts',(-0.54708917182331,-0.115492077056649,
0.85981294420286));
#12024=CARTESIAN_POINT('Ctrl Pts',(-0.560922177770136,-0.141695629206859,
0.850993704737257));
#12025=CARTESIAN_POINT('Ctrl Pts',(-0.590422647829571,-0.181890537957859,
0.830754510485543));
#12026=CARTESIAN_POINT('Ctrl Pts',(-0.609616703125488,-0.201072148666545,
0.816896541396381));
#12027=CARTESIAN_POINT('Ctrl Pts',(-0.641117951819998,-0.223955109275652,
0.792310597819928));
#12028=CARTESIAN_POINT('Ctrl Pts',(-0.657208095763053,-0.232742381310829,
0.779109323683611));
#12029=CARTESIAN_POINT('Ctrl Pts',(-0.68964083160521,-0.244234834628584,
0.750552691816205));
#12030=CARTESIAN_POINT('Ctrl Pts',(-0.705971972091755,-0.246942143572133,
0.735185187071673));
#12031=CARTESIAN_POINT('Ctrl Pts',(-0.735185187071673,-0.246942143572133,
0.705971972091754));
#12032=CARTESIAN_POINT('Ctrl Pts',(-0.750552691816206,-0.244234834628584,
0.689640831605209));
#12033=CARTESIAN_POINT('Ctrl Pts',(-0.779109323683612,-0.232742381310829,
0.657208095763052));
#12034=CARTESIAN_POINT('Ctrl Pts',(-0.792310597819928,-0.223955109275652,
0.641117951819998));
#12035=CARTESIAN_POINT('Ctrl Pts',(-0.816896541396382,-0.201072148666545,
0.609616703125487));
#12036=CARTESIAN_POINT('Ctrl Pts',(-0.830754510485544,-0.181890537957858,
0.590422647829571));
#12037=CARTESIAN_POINT('Ctrl Pts',(-0.850993704737257,-0.141695629206858,
0.560922177770135));
#12038=CARTESIAN_POINT('Ctrl Pts',(-0.859812944202861,-0.115492077056649,
0.547089171823309));
#12039=CARTESIAN_POINT('Ctrl Pts',(-0.868149331745852,-0.0742967091364491,
0.533674141594226));
#12040=CARTESIAN_POINT('Ctrl Pts',(-0.870146645090731,-0.0609922781173483,
0.530395067942936));
#12041=CARTESIAN_POINT('Ctrl Pts',(-0.871530771444223,-0.04763,0.528110872004958));
#12042=CARTESIAN_POINT('',(-0.989696097314,-0.04763,0.242834539687906));
#12043=CARTESIAN_POINT('Origin',(0.,-0.04763,0.));
#12044=CARTESIAN_POINT('',(-1.019052,-0.246942143572133,1.248489836334E-16));
#12045=CARTESIAN_POINT('Ctrl Pts',(-0.989696097314,-0.04763,0.242834539687906));
#12046=CARTESIAN_POINT('Ctrl Pts',(-0.990332542620729,-0.0609922781173483,
0.24024064412003));
#12047=CARTESIAN_POINT('Ctrl Pts',(-0.991238884025248,-0.0742967091364492,
0.236509675094874));
#12048=CARTESIAN_POINT('Ctrl Pts',(-0.994830026707808,-0.115492077056649,
0.221129100087819));
#12049=CARTESIAN_POINT('Ctrl Pts',(-0.998375294985966,-0.141695629206859,
0.205111543747588));
#12050=CARTESIAN_POINT('Ctrl Pts',(-1.00492400591205,-0.181890537957859,
0.169940289819232));
#12051=CARTESIAN_POINT('Ctrl Pts',(-1.00869718865384,-0.201072148666545,
0.1465689792446));
#12052=CARTESIAN_POINT('Ctrl Pts',(-1.01358704779679,-0.223955109275652,
0.106909345252088));
#12053=CARTESIAN_POINT('Ctrl Pts',(-1.0156297872271,-0.232742381310829,
0.0861971848975944));
#12054=CARTESIAN_POINT('Ctrl Pts',(-1.01837060663223,-0.244234834628584,
0.0430711894098825));
#12055=CARTESIAN_POINT('Ctrl Pts',(-1.019052,-0.246942143572133,0.0206568624125608));
#12056=CARTESIAN_POINT('Ctrl Pts',(-1.019052,-0.246942143572133,1.2490009027033E-16));
#12057=CARTESIAN_POINT('',(-1.019052,-0.28578,1.24797876996471E-16));
#12058=CARTESIAN_POINT('',(-1.019052,-0.166705,1.24797876996471E-16));
#12059=CARTESIAN_POINT('Origin',(0.,-0.28578,0.));
#12060=CARTESIAN_POINT('',(-0.989696097314,-0.04763,-0.242834539687906));
#12061=CARTESIAN_POINT('Ctrl Pts',(-1.019052,-0.246942143572133,1.2490009027033E-16));
#12062=CARTESIAN_POINT('Ctrl Pts',(-1.019052,-0.246942143572133,-0.0206568624125605));
#12063=CARTESIAN_POINT('Ctrl Pts',(-1.01837060663223,-0.244234834628584,
-0.0430711894098822));
#12064=CARTESIAN_POINT('Ctrl Pts',(-1.0156297872271,-0.232742381310829,
-0.0861971848975941));
#12065=CARTESIAN_POINT('Ctrl Pts',(-1.01358704779679,-0.223955109275652,
-0.106909345252087));
#12066=CARTESIAN_POINT('Ctrl Pts',(-1.00869718865384,-0.201072148666546,
-0.1465689792446));
#12067=CARTESIAN_POINT('Ctrl Pts',(-1.00492400591205,-0.181890537957859,
-0.169940289819232));
#12068=CARTESIAN_POINT('Ctrl Pts',(-0.998375294985966,-0.141695629206859,
-0.205111543747588));
#12069=CARTESIAN_POINT('Ctrl Pts',(-0.994830026707808,-0.11549207705665,
-0.221129100087819));
#12070=CARTESIAN_POINT('Ctrl Pts',(-0.991238884025248,-0.0742967091364495,
-0.236509675094874));
#12071=CARTESIAN_POINT('Ctrl Pts',(-0.990332542620729,-0.0609922781173484,
-0.24024064412003));
#12072=CARTESIAN_POINT('Ctrl Pts',(-0.989696097314,-0.0476300000000001,
-0.242834539687907));
#12073=CARTESIAN_POINT('',(-0.871530771444223,-0.04763,-0.528110872004958));
#12074=CARTESIAN_POINT('Origin',(0.,-0.04763,0.));
#12075=CARTESIAN_POINT('',(-0.528110872004958,-0.04763,-0.871530771444223));
#12076=CARTESIAN_POINT('Ctrl Pts',(-0.871530771444223,-0.0476300000000001,
-0.528110872004958));
#12077=CARTESIAN_POINT('Ctrl Pts',(-0.87014664509073,-0.0609922781173484,
-0.530395067942936));
#12078=CARTESIAN_POINT('Ctrl Pts',(-0.868149331745851,-0.0742967091364494,
-0.533674141594226));
#12079=CARTESIAN_POINT('Ctrl Pts',(-0.85981294420286,-0.115492077056649,
-0.54708917182331));
#12080=CARTESIAN_POINT('Ctrl Pts',(-0.850993704737257,-0.141695629206859,
-0.560922177770136));
#12081=CARTESIAN_POINT('Ctrl Pts',(-0.830754510485543,-0.181890537957859,
-0.590422647829571));
#12082=CARTESIAN_POINT('Ctrl Pts',(-0.816896541396381,-0.201072148666546,
-0.609616703125488));
#12083=CARTESIAN_POINT('Ctrl Pts',(-0.792310597819928,-0.223955109275652,
-0.641117951819999));
#12084=CARTESIAN_POINT('Ctrl Pts',(-0.779109323683611,-0.232742381310829,
-0.657208095763053));
#12085=CARTESIAN_POINT('Ctrl Pts',(-0.750552691816205,-0.244234834628584,
-0.68964083160521));
#12086=CARTESIAN_POINT('Ctrl Pts',(-0.735185187071673,-0.246942143572133,
-0.705971972091755));
#12087=CARTESIAN_POINT('Ctrl Pts',(-0.705971972091754,-0.246942143572133,
-0.735185187071673));
#12088=CARTESIAN_POINT('Ctrl Pts',(-0.68964083160521,-0.244234834628584,
-0.750552691816206));
#12089=CARTESIAN_POINT('Ctrl Pts',(-0.657208095763052,-0.232742381310829,
-0.779109323683612));
#12090=CARTESIAN_POINT('Ctrl Pts',(-0.641117951819998,-0.223955109275652,
-0.792310597819928));
#12091=CARTESIAN_POINT('Ctrl Pts',(-0.609616703125488,-0.201072148666545,
-0.816896541396381));
#12092=CARTESIAN_POINT('Ctrl Pts',(-0.590422647829571,-0.181890537957859,
-0.830754510485543));
#12093=CARTESIAN_POINT('Ctrl Pts',(-0.560922177770136,-0.141695629206859,
-0.850993704737257));
#12094=CARTESIAN_POINT('Ctrl Pts',(-0.54708917182331,-0.115492077056649,
-0.85981294420286));
#12095=CARTESIAN_POINT('Ctrl Pts',(-0.533674141594226,-0.0742967091364494,
-0.868149331745852));
#12096=CARTESIAN_POINT('Ctrl Pts',(-0.530395067942936,-0.0609922781173484,
-0.870146645090731));
#12097=CARTESIAN_POINT('Ctrl Pts',(-0.528110872004958,-0.0476300000000001,
-0.871530771444223));
#12098=CARTESIAN_POINT('',(-0.242834539687906,-0.04763,-0.989696097314));
#12099=CARTESIAN_POINT('Origin',(0.,-0.04763,0.));
#12100=CARTESIAN_POINT('',(0.242834539687906,-0.04763,-0.989696097314));
#12101=CARTESIAN_POINT('Ctrl Pts',(-0.242834539687907,-0.04763,-0.989696097314));
#12102=CARTESIAN_POINT('Ctrl Pts',(-0.24024064412003,-0.0609922781173483,
-0.990332542620729));
#12103=CARTESIAN_POINT('Ctrl Pts',(-0.236509675094874,-0.0742967091364493,
-0.991238884025248));
#12104=CARTESIAN_POINT('Ctrl Pts',(-0.221129100087819,-0.115492077056649,
-0.994830026707808));
#12105=CARTESIAN_POINT('Ctrl Pts',(-0.205111543747588,-0.141695629206859,
-0.998375294985966));
#12106=CARTESIAN_POINT('Ctrl Pts',(-0.169940289819232,-0.181890537957859,
-1.00492400591205));
#12107=CARTESIAN_POINT('Ctrl Pts',(-0.1465689792446,-0.201072148666545,
-1.00869718865384));
#12108=CARTESIAN_POINT('Ctrl Pts',(-0.106909345252087,-0.223955109275652,
-1.01358704779679));
#12109=CARTESIAN_POINT('Ctrl Pts',(-0.0861971848975942,-0.232742381310829,
-1.0156297872271));
#12110=CARTESIAN_POINT('Ctrl Pts',(-0.0430711894098823,-0.244234834628584,
-1.01837060663223));
#12111=CARTESIAN_POINT('Ctrl Pts',(-0.0206568624125606,-0.246942143572133,
-1.019052));
#12112=CARTESIAN_POINT('Ctrl Pts',(0.0206568624125607,-0.246942143572133,
-1.019052));
#12113=CARTESIAN_POINT('Ctrl Pts',(0.0430711894098824,-0.244234834628584,
-1.01837060663223));
#12114=CARTESIAN_POINT('Ctrl Pts',(0.0861971848975943,-0.232742381310829,
-1.0156297872271));
#12115=CARTESIAN_POINT('Ctrl Pts',(0.106909345252088,-0.223955109275652,
-1.01358704779679));
#12116=CARTESIAN_POINT('Ctrl Pts',(0.1465689792446,-0.201072148666545,-1.00869718865384));
#12117=CARTESIAN_POINT('Ctrl Pts',(0.169940289819232,-0.181890537957859,
-1.00492400591205));
#12118=CARTESIAN_POINT('Ctrl Pts',(0.205111543747588,-0.141695629206859,
-0.998375294985966));
#12119=CARTESIAN_POINT('Ctrl Pts',(0.221129100087819,-0.115492077056649,
-0.994830026707808));
#12120=CARTESIAN_POINT('Ctrl Pts',(0.236509675094874,-0.0742967091364493,
-0.991238884025248));
#12121=CARTESIAN_POINT('Ctrl Pts',(0.24024064412003,-0.0609922781173484,
-0.990332542620729));
#12122=CARTESIAN_POINT('Ctrl Pts',(0.242834539687907,-0.04763,-0.989696097314));
#12123=CARTESIAN_POINT('',(0.528110872004958,-0.04763,-0.871530771444223));
#12124=CARTESIAN_POINT('Origin',(0.,-0.04763,0.));
#12125=CARTESIAN_POINT('',(0.871530771444223,-0.04763,-0.528110872004958));
#12126=CARTESIAN_POINT('Ctrl Pts',(0.528110872004958,-0.0476300000000001,
-0.871530771444223));
#12127=CARTESIAN_POINT('Ctrl Pts',(0.530395067942936,-0.0609922781173484,
-0.870146645090731));
#12128=CARTESIAN_POINT('Ctrl Pts',(0.533674141594226,-0.0742967091364493,
-0.868149331745851));
#12129=CARTESIAN_POINT('Ctrl Pts',(0.54708917182331,-0.115492077056649,
-0.85981294420286));
#12130=CARTESIAN_POINT('Ctrl Pts',(0.560922177770136,-0.141695629206859,
-0.850993704737257));
#12131=CARTESIAN_POINT('Ctrl Pts',(0.590422647829571,-0.181890537957859,
-0.830754510485543));
#12132=CARTESIAN_POINT('Ctrl Pts',(0.609616703125488,-0.201072148666545,
-0.816896541396381));
#12133=CARTESIAN_POINT('Ctrl Pts',(0.641117951819998,-0.223955109275652,
-0.792310597819928));
#12134=CARTESIAN_POINT('Ctrl Pts',(0.657208095763053,-0.232742381310829,
-0.779109323683612));
#12135=CARTESIAN_POINT('Ctrl Pts',(0.68964083160521,-0.244234834628584,
-0.750552691816206));
#12136=CARTESIAN_POINT('Ctrl Pts',(0.705971972091755,-0.246942143572133,
-0.735185187071673));
#12137=CARTESIAN_POINT('Ctrl Pts',(0.735185187071673,-0.246942143572133,
-0.705971972091754));
#12138=CARTESIAN_POINT('Ctrl Pts',(0.750552691816206,-0.244234834628584,
-0.68964083160521));
#12139=CARTESIAN_POINT('Ctrl Pts',(0.779109323683612,-0.232742381310829,
-0.657208095763053));
#12140=CARTESIAN_POINT('Ctrl Pts',(0.792310597819928,-0.223955109275652,
-0.641117951819998));
#12141=CARTESIAN_POINT('Ctrl Pts',(0.816896541396381,-0.201072148666545,
-0.609616703125488));
#12142=CARTESIAN_POINT('Ctrl Pts',(0.830754510485543,-0.181890537957859,
-0.590422647829571));
#12143=CARTESIAN_POINT('Ctrl Pts',(0.850993704737257,-0.141695629206859,
-0.560922177770136));
#12144=CARTESIAN_POINT('Ctrl Pts',(0.85981294420286,-0.115492077056649,
-0.54708917182331));
#12145=CARTESIAN_POINT('Ctrl Pts',(0.868149331745851,-0.0742967091364493,
-0.533674141594226));
#12146=CARTESIAN_POINT('Ctrl Pts',(0.870146645090731,-0.0609922781173484,
-0.530395067942936));
#12147=CARTESIAN_POINT('Ctrl Pts',(0.871530771444223,-0.0476300000000001,
-0.528110872004958));
#12148=CARTESIAN_POINT('',(0.989696097314,-0.04763,-0.242834539687906));
#12149=CARTESIAN_POINT('Origin',(0.,-0.04763,0.));
#12150=CARTESIAN_POINT('',(0.989696097314,-0.04763,0.242834539687906));
#12151=CARTESIAN_POINT('Ctrl Pts',(0.989696097314,-0.04763,-0.242834539687907));
#12152=CARTESIAN_POINT('Ctrl Pts',(0.990332542620729,-0.0609922781173483,
-0.24024064412003));
#12153=CARTESIAN_POINT('Ctrl Pts',(0.991238884025248,-0.0742967091364493,
-0.236509675094874));
#12154=CARTESIAN_POINT('Ctrl Pts',(0.994830026707808,-0.115492077056649,
-0.221129100087819));
#12155=CARTESIAN_POINT('Ctrl Pts',(0.998375294985966,-0.141695629206859,
-0.205111543747588));
#12156=CARTESIAN_POINT('Ctrl Pts',(1.00492400591205,-0.181890537957859,
-0.169940289819232));
#12157=CARTESIAN_POINT('Ctrl Pts',(1.00869718865384,-0.201072148666545,
-0.1465689792446));
#12158=CARTESIAN_POINT('Ctrl Pts',(1.01358704779679,-0.223955109275652,
-0.106909345252087));
#12159=CARTESIAN_POINT('Ctrl Pts',(1.0156297872271,-0.232742381310829,-0.0861971848975942));
#12160=CARTESIAN_POINT('Ctrl Pts',(1.01837060663223,-0.244234834628584,
-0.0430711894098823));
#12161=CARTESIAN_POINT('Ctrl Pts',(1.019052,-0.246942143572133,-0.0206568624125607));
#12162=CARTESIAN_POINT('Ctrl Pts',(1.019052,-0.246942143572133,0.0206568624125607));
#12163=CARTESIAN_POINT('Ctrl Pts',(1.01837060663223,-0.244234834628584,
0.0430711894098823));
#12164=CARTESIAN_POINT('Ctrl Pts',(1.0156297872271,-0.232742381310829,0.0861971848975942));
#12165=CARTESIAN_POINT('Ctrl Pts',(1.01358704779679,-0.223955109275652,
0.106909345252087));
#12166=CARTESIAN_POINT('Ctrl Pts',(1.00869718865384,-0.201072148666545,
0.1465689792446));
#12167=CARTESIAN_POINT('Ctrl Pts',(1.00492400591205,-0.181890537957859,
0.169940289819232));
#12168=CARTESIAN_POINT('Ctrl Pts',(0.998375294985966,-0.141695629206859,
0.205111543747588));
#12169=CARTESIAN_POINT('Ctrl Pts',(0.994830026707808,-0.115492077056649,
0.221129100087819));
#12170=CARTESIAN_POINT('Ctrl Pts',(0.991238884025248,-0.0742967091364492,
0.236509675094874));
#12171=CARTESIAN_POINT('Ctrl Pts',(0.990332542620729,-0.0609922781173483,
0.24024064412003));
#12172=CARTESIAN_POINT('Ctrl Pts',(0.989696097314,-0.04763,0.242834539687907));
#12173=CARTESIAN_POINT('Origin',(0.,-0.04763,0.));
#12174=CARTESIAN_POINT('Origin',(0.,-0.04763,0.));
#12175=CARTESIAN_POINT('',(0.238183666596899,-0.04763,0.951592097314));
#12176=CARTESIAN_POINT('Origin',(0.,-0.04763,0.));
#12177=CARTESIAN_POINT('Origin',(-1.94289029309402E-16,-0.04763,1.));
#12178=CARTESIAN_POINT('Origin',(-1.94289029309402E-16,0.,1.));
#12179=CARTESIAN_POINT('',(-0.2381836665969,-0.04763,0.951592097314));
#12180=CARTESIAN_POINT('Ctrl Pts',(-0.238183666596899,-0.0476299999999999,
0.951592097314));
#12181=CARTESIAN_POINT('Ctrl Pts',(-0.233157223576062,-0.0740444353928835,
0.952850216871763));
#12182=CARTESIAN_POINT('Ctrl Pts',(-0.223801617934946,-0.0999305678883309,
0.955173119738174));
#12183=CARTESIAN_POINT('Ctrl Pts',(-0.199966927975188,-0.142345102874864,
0.960411259488514));
#12184=CARTESIAN_POINT('Ctrl Pts',(-0.1868781821531,-0.159766064500479,
0.963103647174702));
#12185=CARTESIAN_POINT('Ctrl Pts',(-0.15681442133453,-0.190326085855194,
0.968453058988463));
#12186=CARTESIAN_POINT('Ctrl Pts',(-0.139836317888043,-0.203463743702801,
0.971100730005489));
#12187=CARTESIAN_POINT('Ctrl Pts',(-0.104422493053067,-0.224161999508995,
0.975530745318961));
#12188=CARTESIAN_POINT('Ctrl Pts',(-0.0842175114474176,-0.232861760990032,
0.977553872336861));
#12189=CARTESIAN_POINT('Ctrl Pts',(-0.0421062857595701,-0.244251601209411,
0.980270995488453));
#12190=CARTESIAN_POINT('Ctrl Pts',(-0.0201990724523197,-0.246942143572133,
0.980948));
#12191=CARTESIAN_POINT('Ctrl Pts',(0.020199072452319,-0.246942143572133,
0.980948));
#12192=CARTESIAN_POINT('Ctrl Pts',(0.0421062857595694,-0.244251601209411,
0.980270995488454));
#12193=CARTESIAN_POINT('Ctrl Pts',(0.0842175114474169,-0.232861760990032,
0.977553872336861));
#12194=CARTESIAN_POINT('Ctrl Pts',(0.104422493053067,-0.224161999508995,
0.975530745318961));
#12195=CARTESIAN_POINT('Ctrl Pts',(0.139836317888042,-0.203463743702801,
0.971100730005489));
#12196=CARTESIAN_POINT('Ctrl Pts',(0.15681442133453,-0.190326085855194,
0.968453058988463));
#12197=CARTESIAN_POINT('Ctrl Pts',(0.1868781821531,-0.15976606450048,0.963103647174702));
#12198=CARTESIAN_POINT('Ctrl Pts',(0.199966927975188,-0.142345102874864,
0.960411259488514));
#12199=CARTESIAN_POINT('Ctrl Pts',(0.223801617934945,-0.0999305678883309,
0.955173119738174));
#12200=CARTESIAN_POINT('Ctrl Pts',(0.233157223576061,-0.0740444353928835,
0.952850216871763));
#12201=CARTESIAN_POINT('Ctrl Pts',(0.238183666596899,-0.0476299999999999,
0.951592097314));
#12202=CARTESIAN_POINT('Origin',(-1.94289029309402E-16,-0.04763,1.));
#12203=CARTESIAN_POINT('Origin',(0.,-0.04763,0.));
#12204=CARTESIAN_POINT('',(-0.504455939115715,-0.04763,0.841298510752802));
#12205=CARTESIAN_POINT('Origin',(0.,-0.04763,0.));
#12206=CARTESIAN_POINT('Origin',(-0.707106781186548,-0.04763,0.707106781186547));
#12207=CARTESIAN_POINT('Origin',(-0.707106781186548,0.,0.707106781186547));
#12208=CARTESIAN_POINT('',(-0.841298510752802,-0.04763,0.504455939115715));
#12209=CARTESIAN_POINT('Ctrl Pts',(-0.841298510752802,-0.04763,0.504455939115715));
#12210=CARTESIAN_POINT('Ctrl Pts',(-0.838633903678357,-0.0740444353928835,
0.508899795931835));
#12211=CARTESIAN_POINT('Ctrl Pts',(-0.833661031856294,-0.0999305678883309,
0.517157748491652));
#12212=CARTESIAN_POINT('Ctrl Pts',(-0.820511285096538,-0.142345102874864,
0.537715343527944));
#12213=CARTESIAN_POINT('Ctrl Pts',(-0.813159949759,-0.159766064500479,0.548874290046456));
#12214=CARTESIAN_POINT('Ctrl Pts',(-0.795684265985089,-0.190326085855194,
0.573915184558107));
#12215=CARTESIAN_POINT('Ctrl Pts',(-0.78555112003688,-0.203463743702801,
0.587792702767295));
#12216=CARTESIAN_POINT('Ctrl Pts',(-0.763642258217233,-0.224161999508995,
0.615966552324775));
#12217=CARTESIAN_POINT('Ctrl Pts',(-0.750785745543687,-0.232861760990032,
0.631684198665438));
#12218=CARTESIAN_POINT('Ctrl Pts',(-0.722929908501543,-0.244251601209411,
0.663382628119203));
#12219=CARTESIAN_POINT('Ctrl Pts',(-0.707917883896095,-0.246942143572133,
0.679352081686668));
#12220=CARTESIAN_POINT('Ctrl Pts',(-0.679352081686668,-0.246942143572133,
0.707917883896095));
#12221=CARTESIAN_POINT('Ctrl Pts',(-0.663382628119203,-0.244251601209411,
0.722929908501544));
#12222=CARTESIAN_POINT('Ctrl Pts',(-0.631684198665438,-0.232861760990031,
0.750785745543687));
#12223=CARTESIAN_POINT('Ctrl Pts',(-0.615966552324775,-0.224161999508995,
0.763642258217233));
#12224=CARTESIAN_POINT('Ctrl Pts',(-0.587792702767295,-0.203463743702801,
0.78555112003688));
#12225=CARTESIAN_POINT('Ctrl Pts',(-0.573915184558107,-0.190326085855194,
0.795684265985088));
#12226=CARTESIAN_POINT('Ctrl Pts',(-0.548874290046456,-0.159766064500479,
0.813159949759));
#12227=CARTESIAN_POINT('Ctrl Pts',(-0.537715343527944,-0.142345102874864,
0.820511285096538));
#12228=CARTESIAN_POINT('Ctrl Pts',(-0.517157748491652,-0.0999305678883309,
0.833661031856294));
#12229=CARTESIAN_POINT('Ctrl Pts',(-0.508899795931835,-0.0740444353928835,
0.838633903678357));
#12230=CARTESIAN_POINT('Ctrl Pts',(-0.504455939115716,-0.04763,0.841298510752801));
#12231=CARTESIAN_POINT('Origin',(-0.707106781186548,-0.04763,0.707106781186547));
#12232=CARTESIAN_POINT('Origin',(0.,-0.04763,0.));
#12233=CARTESIAN_POINT('',(-0.951592097314,-0.04763,0.238183666596899));
#12234=CARTESIAN_POINT('Origin',(0.,-0.04763,0.));
#12235=CARTESIAN_POINT('Origin',(-1.,-0.04763,-1.11022302462516E-16));
#12236=CARTESIAN_POINT('Origin',(-1.,0.,-1.11022302462516E-16));
#12237=CARTESIAN_POINT('',(-0.951592097314,-0.04763,-0.2381836665969));
#12238=CARTESIAN_POINT('',(-0.980948,-0.246942143572133,1.08514323328844E-18));
#12239=CARTESIAN_POINT('Ctrl Pts',(-0.951592097314,-0.04763,-0.238183666596899));
#12240=CARTESIAN_POINT('Ctrl Pts',(-0.952850216871763,-0.0740444353928835,
-0.233157223576062));
#12241=CARTESIAN_POINT('Ctrl Pts',(-0.955173119738174,-0.0999305678883309,
-0.223801617934946));
#12242=CARTESIAN_POINT('Ctrl Pts',(-0.960411259488514,-0.142345102874864,
-0.199966927975188));
#12243=CARTESIAN_POINT('Ctrl Pts',(-0.963103647174702,-0.159766064500479,
-0.1868781821531));
#12244=CARTESIAN_POINT('Ctrl Pts',(-0.968453058988463,-0.190326085855194,
-0.15681442133453));
#12245=CARTESIAN_POINT('Ctrl Pts',(-0.971100730005489,-0.203463743702801,
-0.139836317888043));
#12246=CARTESIAN_POINT('Ctrl Pts',(-0.975530745318961,-0.224161999508995,
-0.104422493053067));
#12247=CARTESIAN_POINT('Ctrl Pts',(-0.977553872336861,-0.232861760990032,
-0.0842175114474175));
#12248=CARTESIAN_POINT('Ctrl Pts',(-0.980270995488453,-0.244251601209411,
-0.0421062857595699));
#12249=CARTESIAN_POINT('Ctrl Pts',(-0.980948,-0.246942143572133,-0.0201990724523195));
#12250=CARTESIAN_POINT('Ctrl Pts',(-0.980948,-0.246942143572133,-1.17961196366423E-16));
#12251=CARTESIAN_POINT('Origin',(-1.,-0.04763,-1.11022302462516E-16));
#12252=CARTESIAN_POINT('Ctrl Pts',(-0.980948,-0.246942143572133,-1.17961196366423E-16));
#12253=CARTESIAN_POINT('Ctrl Pts',(-0.980948,-0.246942143572133,0.0201990724523192));
#12254=CARTESIAN_POINT('Ctrl Pts',(-0.980270995488453,-0.244251601209411,
0.0421062857595695));
#12255=CARTESIAN_POINT('Ctrl Pts',(-0.977553872336861,-0.232861760990032,
0.0842175114474169));
#12256=CARTESIAN_POINT('Ctrl Pts',(-0.975530745318961,-0.224161999508995,
0.104422493053066));
#12257=CARTESIAN_POINT('Ctrl Pts',(-0.971100730005489,-0.203463743702801,
0.139836317888042));
#12258=CARTESIAN_POINT('Ctrl Pts',(-0.968453058988463,-0.190326085855194,
0.15681442133453));
#12259=CARTESIAN_POINT('Ctrl Pts',(-0.963103647174702,-0.15976606450048,
0.1868781821531));
#12260=CARTESIAN_POINT('Ctrl Pts',(-0.960411259488514,-0.142345102874864,
0.199966927975188));
#12261=CARTESIAN_POINT('Ctrl Pts',(-0.955173119738174,-0.099930567888331,
0.223801617934945));
#12262=CARTESIAN_POINT('Ctrl Pts',(-0.952850216871763,-0.0740444353928835,
0.233157223576061));
#12263=CARTESIAN_POINT('Ctrl Pts',(-0.951592097314,-0.04763,0.238183666596899));
#12264=CARTESIAN_POINT('Origin',(0.,-0.04763,0.));
#12265=CARTESIAN_POINT('',(-0.841298510752802,-0.04763,-0.504455939115715));
#12266=CARTESIAN_POINT('Origin',(0.,-0.04763,0.));
#12267=CARTESIAN_POINT('Origin',(-0.707106781186547,-0.04763,-0.707106781186548));
#12268=CARTESIAN_POINT('Origin',(-0.707106781186547,0.,-0.707106781186548));
#12269=CARTESIAN_POINT('',(-0.504455939115715,-0.04763,-0.841298510752802));
#12270=CARTESIAN_POINT('Ctrl Pts',(-0.504455939115715,-0.04763,-0.841298510752802));
#12271=CARTESIAN_POINT('Ctrl Pts',(-0.508899795931835,-0.0740444353928835,
-0.838633903678357));
#12272=CARTESIAN_POINT('Ctrl Pts',(-0.517157748491652,-0.0999305678883309,
-0.833661031856294));
#12273=CARTESIAN_POINT('Ctrl Pts',(-0.537715343527944,-0.142345102874864,
-0.820511285096538));
#12274=CARTESIAN_POINT('Ctrl Pts',(-0.548874290046456,-0.159766064500479,
-0.813159949759));
#12275=CARTESIAN_POINT('Ctrl Pts',(-0.573915184558107,-0.190326085855194,
-0.795684265985089));
#12276=CARTESIAN_POINT('Ctrl Pts',(-0.587792702767295,-0.203463743702801,
-0.78555112003688));
#12277=CARTESIAN_POINT('Ctrl Pts',(-0.615966552324775,-0.224161999508995,
-0.763642258217233));
#12278=CARTESIAN_POINT('Ctrl Pts',(-0.631684198665438,-0.232861760990032,
-0.750785745543687));
#12279=CARTESIAN_POINT('Ctrl Pts',(-0.663382628119203,-0.244251601209411,
-0.722929908501543));
#12280=CARTESIAN_POINT('Ctrl Pts',(-0.679352081686668,-0.246942143572133,
-0.707917883896095));
#12281=CARTESIAN_POINT('Ctrl Pts',(-0.707917883896095,-0.246942143572133,
-0.679352081686668));
#12282=CARTESIAN_POINT('Ctrl Pts',(-0.722929908501543,-0.244251601209411,
-0.663382628119203));
#12283=CARTESIAN_POINT('Ctrl Pts',(-0.750785745543687,-0.232861760990032,
-0.631684198665439));
#12284=CARTESIAN_POINT('Ctrl Pts',(-0.763642258217232,-0.224161999508995,
-0.615966552324775));
#12285=CARTESIAN_POINT('Ctrl Pts',(-0.78555112003688,-0.203463743702801,
-0.587792702767295));
#12286=CARTESIAN_POINT('Ctrl Pts',(-0.795684265985088,-0.190326085855194,
-0.573915184558107));
#12287=CARTESIAN_POINT('Ctrl Pts',(-0.813159949759,-0.15976606450048,-0.548874290046456));
#12288=CARTESIAN_POINT('Ctrl Pts',(-0.820511285096538,-0.142345102874864,
-0.537715343527944));
#12289=CARTESIAN_POINT('Ctrl Pts',(-0.833661031856294,-0.0999305678883311,
-0.517157748491652));
#12290=CARTESIAN_POINT('Ctrl Pts',(-0.838633903678357,-0.0740444353928836,
-0.508899795931835));
#12291=CARTESIAN_POINT('Ctrl Pts',(-0.841298510752801,-0.04763,-0.504455939115715));
#12292=CARTESIAN_POINT('Origin',(-0.707106781186547,-0.04763,-0.707106781186548));
#12293=CARTESIAN_POINT('Origin',(0.,-0.04763,0.));
#12294=CARTESIAN_POINT('',(-0.238183666596899,-0.04763,-0.951592097314));
#12295=CARTESIAN_POINT('Origin',(0.,-0.04763,0.));
#12296=CARTESIAN_POINT('Origin',(5.55111512312578E-17,-0.04763,-1.));
#12297=CARTESIAN_POINT('Origin',(5.55111512312578E-17,0.,-1.));
#12298=CARTESIAN_POINT('',(0.238183666596899,-0.04763,-0.951592097314));
#12299=CARTESIAN_POINT('Ctrl Pts',(0.238183666596899,-0.04763,-0.951592097314));
#12300=CARTESIAN_POINT('Ctrl Pts',(0.233157223576062,-0.0740444353928835,
-0.952850216871763));
#12301=CARTESIAN_POINT('Ctrl Pts',(0.223801617934946,-0.099930567888331,
-0.955173119738174));
#12302=CARTESIAN_POINT('Ctrl Pts',(0.199966927975188,-0.142345102874864,
-0.960411259488514));
#12303=CARTESIAN_POINT('Ctrl Pts',(0.1868781821531,-0.15976606450048,-0.963103647174702));
#12304=CARTESIAN_POINT('Ctrl Pts',(0.15681442133453,-0.190326085855194,
-0.968453058988463));
#12305=CARTESIAN_POINT('Ctrl Pts',(0.139836317888042,-0.203463743702801,
-0.971100730005489));
#12306=CARTESIAN_POINT('Ctrl Pts',(0.104422493053067,-0.224161999508995,
-0.975530745318961));
#12307=CARTESIAN_POINT('Ctrl Pts',(0.0842175114474173,-0.232861760990032,
-0.977553872336861));
#12308=CARTESIAN_POINT('Ctrl Pts',(0.0421062857595698,-0.244251601209411,
-0.980270995488453));
#12309=CARTESIAN_POINT('Ctrl Pts',(0.0201990724523194,-0.246942143572133,
-0.980948));
#12310=CARTESIAN_POINT('Ctrl Pts',(-0.0201990724523193,-0.246942143572133,
-0.980948));
#12311=CARTESIAN_POINT('Ctrl Pts',(-0.0421062857595697,-0.244251601209411,
-0.980270995488453));
#12312=CARTESIAN_POINT('Ctrl Pts',(-0.0842175114474171,-0.232861760990032,
-0.977553872336861));
#12313=CARTESIAN_POINT('Ctrl Pts',(-0.104422493053067,-0.224161999508995,
-0.975530745318961));
#12314=CARTESIAN_POINT('Ctrl Pts',(-0.139836317888042,-0.203463743702801,
-0.971100730005489));
#12315=CARTESIAN_POINT('Ctrl Pts',(-0.15681442133453,-0.190326085855194,
-0.968453058988463));
#12316=CARTESIAN_POINT('Ctrl Pts',(-0.1868781821531,-0.15976606450048,-0.963103647174702));
#12317=CARTESIAN_POINT('Ctrl Pts',(-0.199966927975188,-0.142345102874864,
-0.960411259488514));
#12318=CARTESIAN_POINT('Ctrl Pts',(-0.223801617934945,-0.099930567888331,
-0.955173119738174));
#12319=CARTESIAN_POINT('Ctrl Pts',(-0.233157223576062,-0.0740444353928835,
-0.952850216871763));
#12320=CARTESIAN_POINT('Ctrl Pts',(-0.238183666596899,-0.0476299999999999,
-0.951592097314));
#12321=CARTESIAN_POINT('Origin',(5.55111512312578E-17,-0.04763,-1.));
#12322=CARTESIAN_POINT('Origin',(0.,-0.04763,0.));
#12323=CARTESIAN_POINT('',(0.504455939115715,-0.04763,-0.841298510752802));
#12324=CARTESIAN_POINT('Origin',(0.,-0.04763,0.));
#12325=CARTESIAN_POINT('Origin',(0.707106781186548,-0.04763,-0.707106781186547));
#12326=CARTESIAN_POINT('Origin',(0.707106781186548,0.,-0.707106781186547));
#12327=CARTESIAN_POINT('',(0.841298510752802,-0.04763,-0.504455939115715));
#12328=CARTESIAN_POINT('Ctrl Pts',(0.841298510752802,-0.04763,-0.504455939115715));
#12329=CARTESIAN_POINT('Ctrl Pts',(0.838633903678357,-0.0740444353928835,
-0.508899795931835));
#12330=CARTESIAN_POINT('Ctrl Pts',(0.833661031856294,-0.0999305678883309,
-0.517157748491652));
#12331=CARTESIAN_POINT('Ctrl Pts',(0.820511285096538,-0.142345102874864,
-0.537715343527944));
#12332=CARTESIAN_POINT('Ctrl Pts',(0.813159949759,-0.159766064500479,-0.548874290046456));
#12333=CARTESIAN_POINT('Ctrl Pts',(0.795684265985088,-0.190326085855194,
-0.573915184558107));
#12334=CARTESIAN_POINT('Ctrl Pts',(0.78555112003688,-0.203463743702801,
-0.587792702767295));
#12335=CARTESIAN_POINT('Ctrl Pts',(0.763642258217233,-0.224161999508995,
-0.615966552324775));
#12336=CARTESIAN_POINT('Ctrl Pts',(0.750785745543687,-0.232861760990032,
-0.631684198665438));
#12337=CARTESIAN_POINT('Ctrl Pts',(0.722929908501543,-0.244251601209411,
-0.663382628119203));
#12338=CARTESIAN_POINT('Ctrl Pts',(0.707917883896095,-0.246942143572133,
-0.679352081686668));
#12339=CARTESIAN_POINT('Ctrl Pts',(0.679352081686668,-0.246942143572133,
-0.707917883896095));
#12340=CARTESIAN_POINT('Ctrl Pts',(0.663382628119203,-0.244251601209411,
-0.722929908501543));
#12341=CARTESIAN_POINT('Ctrl Pts',(0.631684198665438,-0.232861760990032,
-0.750785745543687));
#12342=CARTESIAN_POINT('Ctrl Pts',(0.615966552324775,-0.224161999508995,
-0.763642258217232));
#12343=CARTESIAN_POINT('Ctrl Pts',(0.587792702767295,-0.203463743702801,
-0.78555112003688));
#12344=CARTESIAN_POINT('Ctrl Pts',(0.573915184558107,-0.190326085855194,
-0.795684265985088));
#12345=CARTESIAN_POINT('Ctrl Pts',(0.548874290046456,-0.159766064500479,
-0.813159949759));
#12346=CARTESIAN_POINT('Ctrl Pts',(0.537715343527944,-0.142345102874864,
-0.820511285096538));
#12347=CARTESIAN_POINT('Ctrl Pts',(0.517157748491652,-0.099930567888331,
-0.833661031856294));
#12348=CARTESIAN_POINT('Ctrl Pts',(0.508899795931835,-0.0740444353928835,
-0.838633903678357));
#12349=CARTESIAN_POINT('Ctrl Pts',(0.504455939115715,-0.04763,-0.841298510752801));
#12350=CARTESIAN_POINT('Origin',(0.707106781186548,-0.04763,-0.707106781186547));
#12351=CARTESIAN_POINT('Origin',(0.,-0.166705,0.));
#12352=CARTESIAN_POINT('',(-0.980948,-0.28578,1.20131482833E-16));
#12353=CARTESIAN_POINT('Origin',(0.,-0.28578,0.));
#12354=CARTESIAN_POINT('',(-0.980948,-0.166705,1.20131482833E-16));
#12355=CARTESIAN_POINT('',(0.951592097314,-0.04763,0.238183666596899));
#12356=CARTESIAN_POINT('Origin',(0.,-0.04763,0.));
#12357=CARTESIAN_POINT('',(0.951592097314,-0.04763,-0.238183666596899));
#12358=CARTESIAN_POINT('Ctrl Pts',(0.951592097314,-0.04763,0.238183666596899));
#12359=CARTESIAN_POINT('Ctrl Pts',(0.952850216871763,-0.0740444353928835,
0.233157223576062));
#12360=CARTESIAN_POINT('Ctrl Pts',(0.955173119738174,-0.099930567888331,
0.223801617934945));
#12361=CARTESIAN_POINT('Ctrl Pts',(0.960411259488514,-0.142345102874864,
0.199966927975188));
#12362=CARTESIAN_POINT('Ctrl Pts',(0.963103647174702,-0.15976606450048,
0.1868781821531));
#12363=CARTESIAN_POINT('Ctrl Pts',(0.968453058988463,-0.190326085855194,
0.15681442133453));
#12364=CARTESIAN_POINT('Ctrl Pts',(0.971100730005489,-0.203463743702801,
0.139836317888042));
#12365=CARTESIAN_POINT('Ctrl Pts',(0.975530745318961,-0.224161999508995,
0.104422493053067));
#12366=CARTESIAN_POINT('Ctrl Pts',(0.977553872336861,-0.232861760990032,
0.0842175114474172));
#12367=CARTESIAN_POINT('Ctrl Pts',(0.980270995488453,-0.244251601209411,
0.0421062857595697));
#12368=CARTESIAN_POINT('Ctrl Pts',(0.980948,-0.246942143572133,0.0201990724523194));
#12369=CARTESIAN_POINT('Ctrl Pts',(0.980948,-0.246942143572133,-0.0201990724523194));
#12370=CARTESIAN_POINT('Ctrl Pts',(0.980270995488453,-0.244251601209411,
-0.0421062857595697));
#12371=CARTESIAN_POINT('Ctrl Pts',(0.977553872336861,-0.232861760990032,
-0.0842175114474172));
#12372=CARTESIAN_POINT('Ctrl Pts',(0.975530745318961,-0.224161999508995,
-0.104422493053067));
#12373=CARTESIAN_POINT('Ctrl Pts',(0.971100730005489,-0.203463743702801,
-0.139836317888042));
#12374=CARTESIAN_POINT('Ctrl Pts',(0.968453058988463,-0.190326085855194,
-0.15681442133453));
#12375=CARTESIAN_POINT('Ctrl Pts',(0.963103647174702,-0.15976606450048,
-0.1868781821531));
#12376=CARTESIAN_POINT('Ctrl Pts',(0.960411259488514,-0.142345102874864,
-0.199966927975188));
#12377=CARTESIAN_POINT('Ctrl Pts',(0.955173119738174,-0.099930567888331,
-0.223801617934945));
#12378=CARTESIAN_POINT('Ctrl Pts',(0.952850216871763,-0.0740444353928835,
-0.233157223576062));
#12379=CARTESIAN_POINT('Ctrl Pts',(0.951592097314,-0.0476299999999999,-0.238183666596899));
#12380=CARTESIAN_POINT('Origin',(0.,-0.04763,0.));
#12381=CARTESIAN_POINT('Origin',(0.,-0.04763,0.));
#12382=CARTESIAN_POINT('Origin',(1.,-0.04763,0.));
#12383=CARTESIAN_POINT('Origin',(1.,0.,0.));
#12384=CARTESIAN_POINT('Origin',(1.,-0.04763,0.));
#12385=CARTESIAN_POINT('Origin',(0.,-0.28578,0.));
#12386=CARTESIAN_POINT('Origin',(0.,-0.04763,0.));
#12727=UNCERTAINTY_MEASURE_WITH_UNIT(LENGTH_MEASURE(0.001),#12784,
'DISTANCE_ACCURACY_VALUE',
'Maximum model space distance between geometric entities at asserted c
onnectivities');
#12739=UNCERTAINTY_MEASURE_WITH_UNIT(LENGTH_MEASURE(0.001),#12784,
'DISTANCE_ACCURACY_VALUE',
'Maximum model space distance between geometric entities at asserted c
onnectivities');
#12771=(
GEOMETRIC_REPRESENTATION_CONTEXT(3)
GLOBAL_UNCERTAINTY_ASSIGNED_CONTEXT((#12727))
GLOBAL_UNIT_ASSIGNED_CONTEXT((#12784,#12786,#12787))
REPRESENTATION_CONTEXT('','3D')
);
#12783=(
GEOMETRIC_REPRESENTATION_CONTEXT(3)
GLOBAL_UNCERTAINTY_ASSIGNED_CONTEXT((#12739))
GLOBAL_UNIT_ASSIGNED_CONTEXT((#12784,#12786,#12787))
REPRESENTATION_CONTEXT('','3D')
);
#12784=(
LENGTH_UNIT()
NAMED_UNIT(*)
SI_UNIT(.CENTI.,.METRE.)
);
#12786=(
NAMED_UNIT(*)
PLANE_ANGLE_UNIT()
SI_UNIT($,.RADIAN.)
);
#12787=(
NAMED_UNIT(*)
SI_UNIT($,.STERADIAN.)
SOLID_ANGLE_UNIT()
);
#12819=SHAPE_DEFINITION_REPRESENTATION(#12888,#12962);
#12888=PRODUCT_DEFINITION_SHAPE('',$,#13006);
#12962=SHAPE_REPRESENTATION('',(#7595),#12771);
#12974=PRODUCT_DEFINITION_CONTEXT('part definition',#13105,'design');
#13006=PRODUCT_DEFINITION('Cage (1)','Cage (1)',#13049,#12974);
#13049=PRODUCT_DEFINITION_FORMATION('',$,#13138);
#13105=APPLICATION_CONTEXT(
'Core Data for Automotive Mechanical Design Process');
#13106=PRODUCT_CONTEXT('part definition',#13105,'mechanical');
#13138=PRODUCT('Cage (1)','Cage (1)','Cage (1)',(#13106));
#13206=COLOUR_RGB('Grey',0.48,0.52,0.57);
#13207=FILL_AREA_STYLE_COLOUR('',#13206);
#13208=FILL_AREA_STYLE('',(#13207));
#13209=SURFACE_STYLE_FILL_AREA(#13208);
#13210=SURFACE_SIDE_STYLE('',(#13209));
#13211=SURFACE_STYLE_USAGE(.BOTH.,#13210);
#13212=PRESENTATION_STYLE_ASSIGNMENT((#13211));
ENDSEC;
END-ISO-10303-21;
